ISO-10303-21;
HEADER;
FILE_DESCRIPTION (('STEP AP214'),
    '1' );
FILE_NAME ('spur gear_iso_ISO - Spur gear 3M 16T 20PA 5FW ---S16A75H50L10.0S1.step',
    '2026-10-27T08:02:39',
    ( '' ),
    ( '' ),
    'SwSTEP 2.0',
    'SolidWorks 2026',
    '' );
FILE_SCHEMA (( 'AUTOMOTIVE_DESIGN' ));
ENDSEC;

DATA;
#4=AXIS2_PLACEMENT_3D ( 'NONE', #1352, #1240, #9072 ) ;
#5=CARTESIAN_POINT ( 'NONE',  ( 0.000000000000000000, -11.14352537685160982, -19.60720892790264713 ) ) ;
#7=ORIENTED_EDGE ( 'NONE', *, *, #8174, .F. ) ;
#13=ORIENTED_EDGE ( 'NONE', *, *, #11735, .F. ) ;
#22=DIRECTION ( 'NONE',  ( -1.000000000000000000, 0.000000000000000000, 0.000000000000000000 ) ) ;
#23=FACE_BOUND ( 'NONE', #5725, .T. ) ;
#25=CIRCLE ( 'NONE', #9413, 20.24900000002024925 ) ;
#30=AXIS2_PLACEMENT_3D ( 'NONE', #1488, #11904, #1413 ) ;
#39=AXIS2_PLACEMENT_3D ( 'NONE', #8335, #2568, #9339 ) ;
#40=ORIENTED_EDGE ( 'NONE', *, *, #10982, .T. ) ;
#41=AXIS2_PLACEMENT_3D ( 'NONE', #9780, #4085, #382 ) ;
#43=ORIENTED_EDGE ( 'NONE', *, *, #3948, .F. ) ;
#44=CARTESIAN_POINT ( 'NONE',  ( 4.999999999999999112, 22.37914155802281257, 2.791921004064645384 ) ) ;
#48=ORIENTED_EDGE ( 'NONE', *, *, #3948, .T. ) ;
#50=CYLINDRICAL_SURFACE ( 'NONE', #10960, 20.24900000002024569 ) ;
#53=CIRCLE ( 'NONE', #7047, 9.600000000009602630 ) ;
#60=EDGE_CURVE ( 'NONE', #6322, #1163, #6180, .T. ) ;
#64=VECTOR ( 'NONE', #5535, 1000.000000000000000 ) ;
#67=DIRECTION ( 'NONE',  ( 0.000000000000000000, 0.000000000000000000, -1.000000000000000000 ) ) ;
#69=ORIENTED_EDGE ( 'NONE', *, *, #8618, .F. ) ;
#70=LINE ( 'NONE', #2883, #8880 ) ;
#75=AXIS2_PLACEMENT_3D ( 'NONE', #10633, #5941, #1246 ) ;
#78=EDGE_CURVE ( 'NONE', #474, #1066, #6869, .T. ) ;
#81=CARTESIAN_POINT ( 'NONE',  ( 2.499999999999999556, 22.05152472667151642, -15.57980286237449619 ) ) ;
#83=LINE ( 'NONE', #947, #2363 ) ;
#95=ORIENTED_EDGE ( 'NONE', *, *, #5318, .F. ) ;
#102=VERTEX_POINT ( 'NONE', #11771 ) ;
#104=DIRECTION ( 'NONE',  ( -1.000000000000000000, -0.000000000000000000, 0.000000000000000000 ) ) ;
#112=ADVANCED_FACE ( 'NONE', ( #8980 ), #4043, .T. ) ;
#119=EDGE_CURVE ( 'NONE', #4367, #3187, #6988, .T. ) ;
#121=DIRECTION ( 'NONE',  ( 0.000000000000000000, 0.000000000000000000, 1.000000000000000000 ) ) ;
#137=LINE ( 'NONE', #2829, #1850 ) ;
#138=VERTEX_POINT ( 'NONE', #7349 ) ;
#144=ORIENTED_EDGE ( 'NONE', *, *, #7851, .F. ) ;
#148=EDGE_CURVE ( 'NONE', #6125, #9230, #7162, .T. ) ;
#149=DIRECTION ( 'NONE',  ( 0.000000000000000000, 0.000000000000000000, 1.000000000000000000 ) ) ;
#151=ORIENTED_EDGE ( 'NONE', *, *, #5543, .T. ) ;
#157=ORIENTED_EDGE ( 'NONE', *, *, #3999, .F. ) ;
#165=EDGE_LOOP ( 'NONE', ( #11428, #11250, #3782, #590 ) ) ;
#174=EDGE_CURVE ( 'NONE', #11053, #10042, #2785, .T. ) ;
#175=CIRCLE ( 'NONE', #11932, 27.00000000002699707 ) ;
#177=CLOSED_SHELL ( 'NONE', ( #10284, #2336, #8766, #4424, #8491, #9078, #4920, #2783, #9249, #727, #1702, #2014, #7994, #8544, #7366, #12201, #5608, #5505, #10582, #11708, #6045, #8749, #2274, #6335, #7524, #5095, #6706, #112, #3625, #728, #7634, #6314, #6863, #8461, #9912, #6936, #3075, #7445, #11950, #5150, #5319, #7411, #10495, #2256, #1343, #9815, #12107, #8150, #5564, #11571, #10132, #3776, #7922, #4726, #8290, #2161, #3112, #11868, #8305, #4757, #8516, #1346, #525, #10969, #10935, #8135, #12114, #7185, #9760, #8007, #2667, #5107, #4369, #5486, #6938, #820, #1296 ) ) ;
#180=ORIENTED_EDGE ( 'NONE', *, *, #4930, .T. ) ;
#183=CARTESIAN_POINT ( 'NONE',  ( 0.000000000000000000, -22.05152472667118957, -15.57980286237495626 ) ) ;
#186=FACE_OUTER_BOUND ( 'NONE', #7398, .T. ) ;
#189=EDGE_CURVE ( 'NONE', #3572, #7704, #8788, .T. ) ;
#190=AXIS2_PLACEMENT_3D ( 'NONE', #3113, #5922, #4971 ) ;
#199=DIRECTION ( 'NONE',  ( -1.000000000000000000, -0.000000000000000000, 0.000000000000000000 ) ) ;
#201=AXIS2_PLACEMENT_3D ( 'NONE', #9324, #9448, #3624 ) ;
#206=VECTOR ( 'NONE', #6495, 1000.000000000000000 ) ;
#208=CARTESIAN_POINT ( 'NONE',  ( 0.000000000000000000, -5.984728032765115557, 21.74405275335756116 ) ) ;
#212=CARTESIAN_POINT ( 'NONE',  ( 0.000000000000000000, 0.000000000000000000, 0.000000000000000000 ) ) ;
#217=ORIENTED_EDGE ( 'NONE', *, *, #2945, .T. ) ;
#222=AXIS2_PLACEMENT_3D ( 'NONE', #3797, #9085, #2730 ) ;
#224=AXIS2_PLACEMENT_3D ( 'NONE', #1139, #4013, #1014 ) ;
#225=FACE_OUTER_BOUND ( 'NONE', #3091, .T. ) ;
#232=ORIENTED_EDGE ( 'NONE', *, *, #10676, .F. ) ;
#234=ORIENTED_EDGE ( 'NONE', *, *, #9201, .F. ) ;
#237=AXIS2_PLACEMENT_3D ( 'NONE', #4529, #4405, #8346 ) ;
#238=VERTEX_POINT ( 'NONE', #12026 ) ;
#239=DIRECTION ( 'NONE',  ( -1.000000000000000000, 0.000000000000000000, 0.000000000000000000 ) ) ;
#241=CARTESIAN_POINT ( 'NONE',  ( 0.000000000000000000, -21.74405275335762155, 15.58472803277448726 ) ) ;
#245=CIRCLE ( 'NONE', #10429, 20.24900000002024569 ) ;
#246=DIRECTION ( 'NONE',  ( -1.000000000000000000, -0.000000000000000000, -0.000000000000000000 ) ) ;
#253=EDGE_LOOP ( 'NONE', ( #7852, #10617, #12284, #5866 ) ) ;
#262=DIRECTION ( 'NONE',  ( -1.000000000000000000, 0.000000000000000000, 0.000000000000000000 ) ) ;
#263=DIRECTION ( 'NONE',  ( -1.000000000000000000, 0.000000000000000000, 0.000000000000000000 ) ) ;
#266=CARTESIAN_POINT ( 'NONE',  ( 0.000000000000000000, 22.83261415639523406, -14.41081992069285000 ) ) ;
#275=CYLINDRICAL_SURFACE ( 'NONE', #8197, 9.600000000009600853 ) ;
#288=ORIENTED_EDGE ( 'NONE', *, *, #12313, .F. ) ;
#289=ORIENTED_EDGE ( 'NONE', *, *, #4474, .F. ) ;
#291=DIRECTION ( 'NONE',  ( 0.000000000000000000, 0.000000000000000000, -1.000000000000000000 ) ) ;
#301=DIRECTION ( 'NONE',  ( -1.000000000000000000, 0.000000000000000000, -0.000000000000000000 ) ) ;
#304=AXIS2_PLACEMENT_3D ( 'NONE', #9190, #8313, #6184 ) ;
#306=CARTESIAN_POINT ( 'NONE',  ( 0.000000000000000000, 0.000000000000000000, 0.000000000000000000 ) ) ;
#308=ORIENTED_EDGE ( 'NONE', *, *, #687, .F. ) ;
#318=CARTESIAN_POINT ( 'NONE',  ( 0.000000000000000000, 0.000000000000000000, 0.000000000000000000 ) ) ;
#323=DIRECTION ( 'NONE',  ( 0.000000000000000000, 0.000000000000000000, 1.000000000000000000 ) ) ;
#325=DIRECTION ( 'NONE',  ( -1.000000000000000000, -0.000000000000000000, -0.000000000000000000 ) ) ;
#338=DIRECTION ( 'NONE',  ( 0.000000000000000000, 0.000000000000000000, 1.000000000000000000 ) ) ;
#343=EDGE_CURVE ( 'NONE', #6998, #4367, #6189, .T. ) ;
#347=ORIENTED_EDGE ( 'NONE', *, *, #6557, .F. ) ;
#350=CARTESIAN_POINT ( 'NONE',  ( 4.999999999999999112, 0.000000000000000000, 0.000000000000000000 ) ) ;
#351=FACE_OUTER_BOUND ( 'NONE', #1653, .T. ) ;
#354=DIRECTION ( 'NONE',  ( -1.000000000000000000, -0.000000000000000000, -0.000000000000000000 ) ) ;
#356=AXIS2_PLACEMENT_3D ( 'NONE', #9265, #12164, #12106 ) ;
#357=ORIENTED_EDGE ( 'NONE', *, *, #3489, .F. ) ;
#360=DIRECTION ( 'NONE',  ( 0.000000000000000000, 0.000000000000000000, 1.000000000000000000 ) ) ;
#370=DIRECTION ( 'NONE',  ( 0.000000000000000000, 0.3826834323650840641, 0.9238795325112890700 ) ) ;
#376=CARTESIAN_POINT ( 'NONE',  ( 4.999999999999999112, -13.85025647830044271, -17.79862902732279650 ) ) ;
#382=DIRECTION ( 'NONE',  ( 0.000000000000000000, 0.9238795325112878487, -0.3826834323650872283 ) ) ;
#390=ORIENTED_EDGE ( 'NONE', *, *, #3924, .T. ) ;
#404=VECTOR ( 'NONE', #11917, 1000.000000000000000 ) ;
#411=DIRECTION ( 'NONE',  ( -1.000000000000000000, 0.000000000000000000, 0.000000000000000000 ) ) ;
#414=EDGE_CURVE ( 'NONE', #11497, #7805, #1388, .T. ) ;
#419=FACE_OUTER_BOUND ( 'NONE', #4196, .T. ) ;
#422=AXIS2_PLACEMENT_3D ( 'NONE', #6109, #1403, #7981 ) ;
#424=AXIS2_PLACEMENT_3D ( 'NONE', #3329, #7021, #7141 ) ;
#425=( LENGTH_UNIT ( ) NAMED_UNIT ( * ) SI_UNIT ( .MILLI., .METRE. ) );
#453=AXIS2_PLACEMENT_3D ( 'NONE', #10970, #2408, #533 ) ;
#457=AXIS2_PLACEMENT_3D ( 'NONE', #6194, #7953, #1192 ) ;
#460=DIRECTION ( 'NONE',  ( -1.000000000000000000, -0.000000000000000000, 0.000000000000000000 ) ) ;
#462=ORIENTED_EDGE ( 'NONE', *, *, #746, .F. ) ;
#463=EDGE_CURVE ( 'NONE', #1857, #10975, #10577, .T. ) ;
#469=DIRECTION ( 'NONE',  ( 0.000000000000000000, 0.000000000000000000, 1.000000000000000000 ) ) ;
#474=VERTEX_POINT ( 'NONE', #3689 ) ;
#479=ORIENTED_EDGE ( 'NONE', *, *, #9679, .F. ) ;
#486=VERTEX_POINT ( 'NONE', #7507 ) ;
#492=CARTESIAN_POINT ( 'NONE',  ( 50.00005079999999680, 6.799999999999999822, 1.500000000000000000 ) ) ;
#509=DIRECTION ( 'NONE',  ( -1.000000000000000000, -0.000000000000000000, -0.000000000000000000 ) ) ;
#515=CARTESIAN_POINT ( 'NONE',  ( 0.000000000000000000, 0.000000000000000000, 0.000000000000000000 ) ) ;
#518=ORIENTED_EDGE ( 'NONE', *, *, #8114, .T. ) ;
#525=ADVANCED_FACE ( 'NONE', ( #2684 ), #3746, .T. ) ;
#526=DIRECTION ( 'NONE',  ( -1.000000000000000000, -0.000000000000000000, -0.000000000000000000 ) ) ;
#529=DIRECTION ( 'NONE',  ( -1.000000000000000000, -0.000000000000000000, 0.000000000000000000 ) ) ;
#533=DIRECTION ( 'NONE',  ( 0.000000000000000000, 0.000000000000000000, 1.000000000000000000 ) ) ;
#536=VERTEX_POINT ( 'NONE', #4438 ) ;
#537=DIRECTION ( 'NONE',  ( -1.000000000000000000, -0.000000000000000000, -0.000000000000000000 ) ) ;
#546=DIRECTION ( 'NONE',  ( 0.000000000000000000, -0.3826834323650971093, 0.9238795325112837409 ) ) ;
#555=DIRECTION ( 'NONE',  ( 0.000000000000000000, -0.9238795325112906243, 0.3826834323650805669 ) ) ;
#561=ORIENTED_EDGE ( 'NONE', *, *, #3933, .T. ) ;
#563=CIRCLE ( 'NONE', #1979, 9.600000000009600853 ) ;
#564=AXIS2_PLACEMENT_3D ( 'NONE', #1557, #9139, #10182 ) ;
#568=CARTESIAN_POINT ( 'NONE',  ( 2.499999999999999556, -26.33508479058316709, -5.955107813822780649 ) ) ;
#576=ORIENTED_EDGE ( 'NONE', *, *, #10600, .F. ) ;
#578=ORIENTED_EDGE ( 'NONE', *, *, #2670, .T. ) ;
#580=CIRCLE ( 'NONE', #2188, 20.24900000002024569 ) ;
#581=DIRECTION ( 'NONE',  ( -1.000000000000000000, 0.000000000000000000, 0.000000000000000000 ) ) ;
#582=AXIS2_PLACEMENT_3D ( 'NONE', #7871, #10854, #2285 ) ;
#584=DIRECTION ( 'NONE',  ( -1.000000000000000000, 0.000000000000000000, 0.000000000000000000 ) ) ;
#585=DIRECTION ( 'NONE',  ( -1.000000000000000000, 0.000000000000000000, 0.000000000000000000 ) ) ;
#587=EDGE_LOOP ( 'NONE', ( #7114, #3255, #8171, #7068, #1098, #2370 ) ) ;
#590=ORIENTED_EDGE ( 'NONE', *, *, #9258, .F. ) ;
#594=ORIENTED_EDGE ( 'NONE', *, *, #7647, .F. ) ;
#597=DIRECTION ( 'NONE',  ( 0.000000000000000000, -6.866613759067995433E-15, 1.000000000000000000 ) ) ;
#610=CIRCLE ( 'NONE', #7014, 9.600000000009600853 ) ;
#612=DIRECTION ( 'NONE',  ( -1.000000000000000000, -0.000000000000000000, 0.000000000000000000 ) ) ;
#621=FACE_OUTER_BOUND ( 'NONE', #9304, .T. ) ;
#623=ORIENTED_EDGE ( 'NONE', *, *, #10422, .F. ) ;
#624=ORIENTED_EDGE ( 'NONE', *, *, #2786, .T. ) ;
#626=DIRECTION ( 'NONE',  ( -1.000000000000000000, -0.000000000000000000, 0.000000000000000000 ) ) ;
#628=DIRECTION ( 'NONE',  ( -1.000000000000000000, -0.000000000000000000, -0.000000000000000000 ) ) ;
#633=AXIS2_PLACEMENT_3D ( 'NONE', #8324, #9459, #7388 ) ;
#634=AXIS2_PLACEMENT_3D ( 'NONE', #5026, #9910, #7099 ) ;
#636=( LENGTH_UNIT ( ) NAMED_UNIT ( * ) SI_UNIT ( .MILLI., .METRE. ) );
#637=DIRECTION ( 'NONE',  ( -1.000000000000000000, 0.000000000000000000, -0.000000000000000000 ) ) ;
#639=STYLED_ITEM ( 'NONE', ( #8368 ), #8868 ) ;
#640=CARTESIAN_POINT ( 'NONE',  ( 0.000000000000000000, 0.000000000000000000, 0.000000000000000000 ) ) ;
#644=VERTEX_POINT ( 'NONE', #241 ) ;
#645=EDGE_CURVE ( 'NONE', #3502, #9875, #4601, .T. ) ;
#653=AXIS2_PLACEMENT_3D ( 'NONE', #10130, #1625, #8195 ) ;
#665=DIRECTION ( 'NONE',  ( -1.000000000000000000, 0.000000000000000000, 0.000000000000000000 ) ) ;
#666=EDGE_CURVE ( 'NONE', #12146, #7642, #10385, .T. ) ;
#673=CARTESIAN_POINT ( 'NONE',  ( 4.999999999999999112, -22.83261415639492142, -14.41081992069334028 ) ) ;
#675=DIRECTION ( 'NONE',  ( 0.000000000000000000, 0.000000000000000000, 1.000000000000000000 ) ) ;
#687=EDGE_CURVE ( 'NONE', #7798, #6404, #4400, .T. ) ;
#690=ORIENTED_EDGE ( 'NONE', *, *, #8695, .T. ) ;
#697=ORIENTED_EDGE ( 'NONE', *, *, #12266, .F. ) ;
#700=DIRECTION ( 'NONE',  ( -1.000000000000000000, 0.000000000000000000, -0.000000000000000000 ) ) ;
#703=DIRECTION ( 'NONE',  ( -1.000000000000000000, -0.000000000000000000, 0.000000000000000000 ) ) ;
#717=FACE_OUTER_BOUND ( 'NONE', #8562, .T. ) ;
#719=DIRECTION ( 'NONE',  ( -1.000000000000000000, 0.000000000000000000, -0.000000000000000000 ) ) ;
#727=ADVANCED_FACE ( 'NONE', ( #351 ), #5059, .F. ) ;
#728=ADVANCED_FACE ( 'NONE', ( #419 ), #10867, .T. ) ;
#729=ORIENTED_EDGE ( 'NONE', *, *, #1755, .F. ) ;
#736=DIRECTION ( 'NONE',  ( 0.000000000000000000, 0.000000000000000000, 1.000000000000000000 ) ) ;
#742=ORIENTED_EDGE ( 'NONE', *, *, #4488, .F. ) ;
#745=DIRECTION ( 'NONE',  ( 0.000000000000000000, 0.000000000000000000, 1.000000000000000000 ) ) ;
#746=EDGE_CURVE ( 'NONE', #8081, #1083, #9126, .T. ) ;
#747=ORIENTED_EDGE ( 'NONE', *, *, #7161, .T. ) ;
#753=DIRECTION ( 'NONE',  ( 0.000000000000000000, 8.881784197001252323E-16, 1.000000000000000000 ) ) ;
#759=ORIENTED_EDGE ( 'NONE', *, *, #9853, .T. ) ;
#760=CARTESIAN_POINT ( 'NONE',  ( 0.000000000000000000, -22.37914155802283034, 6.808078995945121115 ) ) ;
#768=CARTESIAN_POINT ( 'NONE',  ( 4.999999999999999112, 15.37949036966211835, 13.17168466712934105 ) ) ;
#769=DIRECTION ( 'NONE',  ( 1.000000000000000000, 0.000000000000000000, 0.000000000000000000 ) ) ;
#772=CARTESIAN_POINT ( 'NONE',  ( 4.999999999999999112, -19.24938187143300539, 6.283573709965241783 ) ) ;
#783=CARTESIAN_POINT ( 'NONE',  ( 4.999999999999999112, 9.168210874537823685, -18.05452603534156353 ) ) ;
#784=CARTESIAN_POINT ( 'NONE',  ( 4.999999999999999112, 1.561154383803505796, -20.18872947935929574 ) ) ;
#786=ORIENTED_EDGE ( 'NONE', *, *, #9903, .T. ) ;
#788=DIRECTION ( 'NONE',  ( 0.000000000000000000, 0.000000000000000000, 1.000000000000000000 ) ) ;
#800=AXIS2_PLACEMENT_3D ( 'NONE', #10645, #2078, #1132 ) ;
#806=CARTESIAN_POINT ( 'NONE',  ( 4.999999999999999112, 11.14352537685174660, 19.60720892790256897 ) ) ;
#810=CARTESIAN_POINT ( 'NONE',  ( 4.999999999999999112, -1.561154383803080581, -20.18872947935932771 ) ) ;
#813=AXIS2_PLACEMENT_3D ( 'NONE', #11633, #7898, #11689 ) ;
#815=AXIS2_PLACEMENT_3D ( 'NONE', #1986, #6874, #10541 ) ;
#816=VECTOR ( 'NONE', #12136, 1000.000000000000000 ) ;
#817=VECTOR ( 'NONE', #8993, 1000.000000000000000 ) ;
#818=DIRECTION ( 'NONE',  ( -1.000000000000000000, -0.000000000000000000, 0.000000000000000000 ) ) ;
#820=ADVANCED_FACE ( 'NONE', ( #1492 ), #6175, .T. ) ;
#831=CIRCLE ( 'NONE', #11809, 9.600000000009600853 ) ;
#834=CIRCLE ( 'NONE', #4220, 20.24900000002024569 ) ;
#838=CARTESIAN_POINT ( 'NONE',  ( 4.999999999999999112, 0.000000000000000000, 0.000000000000000000 ) ) ;
#845=ORIENTED_EDGE ( 'NONE', *, *, #3771, .T. ) ;
#848=DIRECTION ( 'NONE',  ( -1.000000000000000000, 0.000000000000000000, 0.000000000000000000 ) ) ;
#850=EDGE_LOOP ( 'NONE', ( #7886, #4697, #10680, #9743 ) ) ;
#852=VECTOR ( 'NONE', #909, 1000.000000000000000 ) ;
#854=DIRECTION ( 'NONE',  ( -1.000000000000000000, 0.000000000000000000, 0.000000000000000000 ) ) ;
#874=ORIENTED_EDGE ( 'NONE', *, *, #4487, .F. ) ;
#883=EDGE_CURVE ( 'NONE', #6238, #3985, #11291, .T. ) ;
#886=EDGE_CURVE ( 'NONE', #1449, #11926, #6396, .T. ) ;
#890=CARTESIAN_POINT ( 'NONE',  ( 4.999999999999999112, -14.41081992069325679, 22.83261415639497471 ) ) ;
#891=LINE ( 'NONE', #5758, #6852 ) ;
#895=ORIENTED_EDGE ( 'NONE', *, *, #9149, .F. ) ;
#898=CIRCLE ( 'NONE', #10278, 9.600000000009600853 ) ;
#902=CARTESIAN_POINT ( 'NONE',  ( 2.499999999999999556, 22.05152472667129970, 15.57980286237480172 ) ) ;
#904=AXIS2_PLACEMENT_3D ( 'NONE', #4247, #10925, #2491 ) ;
#906=FACE_OUTER_BOUND ( 'NONE', #10491, .T. ) ;
#908=VERTEX_POINT ( 'NONE', #5430 ) ;
#909=DIRECTION ( 'NONE',  ( -1.000000000000000000, 0.000000000000000000, 0.000000000000000000 ) ) ;
#910=ORIENTED_EDGE ( 'NONE', *, *, #7161, .F. ) ;
#915=FACE_OUTER_BOUND ( 'NONE', #11711, .T. ) ;
#918=ORIENTED_EDGE ( 'NONE', *, *, #7157, .T. ) ;
#923=DIRECTION ( 'NONE',  ( -1.000000000000000000, 0.000000000000000000, 0.000000000000000000 ) ) ;
#925=FILL_AREA_STYLE_COLOUR ( '', #9637 ) ;
#926=ORIENTED_EDGE ( 'NONE', *, *, #1803, .F. ) ;
#930=CARTESIAN_POINT ( 'NONE',  ( 0.000000000000000000, 0.000000000000000000, 0.000000000000000000 ) ) ;
#937=CARTESIAN_POINT ( 'NONE',  ( 4.999999999999999112, -17.79862902732275032, 13.85025647830051021 ) ) ;
#942=DIRECTION ( 'NONE',  ( 0.000000000000000000, 0.000000000000000000, 1.000000000000000000 ) ) ;
#947=CARTESIAN_POINT ( 'NONE',  ( 4.999999999999999112, -22.37914155802283034, 6.808078995945121115 ) ) ;
#965=EDGE_CURVE ( 'NONE', #9862, #8991, #4609, .T. ) ;
#970=AXIS2_PLACEMENT_3D ( 'NONE', #8936, #4115, #7935 ) ;
#978=VERTEX_POINT ( 'NONE', #783 ) ;
#979=EDGE_CURVE ( 'NONE', #3276, #5514, #4817, .T. ) ;
#982=CIRCLE ( 'NONE', #4170, 9.600000000009599077 ) ;
#985=( NAMED_UNIT ( * ) SI_UNIT ( $, .STERADIAN. ) SOLID_ANGLE_UNIT ( ) );
#986=ORIENTED_EDGE ( 'NONE', *, *, #11375, .F. ) ;
#992=VECTOR ( 'NONE', #7075, 1000.000000000000000 ) ;
#997=VERTEX_POINT ( 'NONE', #8434 ) ;
#1001=AXIS2_PLACEMENT_3D ( 'NONE', #7684, #2154, #6925 ) ;
#1014=DIRECTION ( 'NONE',  ( 0.000000000000000000, 0.000000000000000000, 1.000000000000000000 ) ) ;
#1015=ORIENTED_EDGE ( 'NONE', *, *, #10828, .F. ) ;
#1016=LINE ( 'NONE', #10518, #4484 ) ;
#1020=CIRCLE ( 'NONE', #2215, 9.600000000009599077 ) ;
#1022=AXIS2_PLACEMENT_3D ( 'NONE', #5166, #4230, #8124 ) ;
#1030=CARTESIAN_POINT ( 'NONE',  ( 4.999999999999999112, 0.000000000000000000, 0.000000000000000000 ) ) ;
#1031=CIRCLE ( 'NONE', #9223, 5.000000000000000000 ) ;
#1032=VERTEX_POINT ( 'NONE', #6872 ) ;
#1034=CIRCLE ( 'NONE', #2618, 9.600000000009602630 ) ;
#1043=ORIENTED_EDGE ( 'NONE', *, *, #2786, .F. ) ;
#1055=CIRCLE ( 'NONE', #10045, 9.600000000009600853 ) ;
#1062=DIRECTION ( 'NONE',  ( -1.000000000000000000, 0.000000000000000000, 0.000000000000000000 ) ) ;
#1066=VERTEX_POINT ( 'NONE', #3977 ) ;
#1067=CYLINDRICAL_SURFACE ( 'NONE', #4355, 9.600000000009600853 ) ;
#1073=VECTOR ( 'NONE', #6944, 1000.000000000000000 ) ;
#1082=DIRECTION ( 'NONE',  ( 1.000000000000000000, -0.000000000000000000, -0.000000000000000000 ) ) ;
#1083=VERTEX_POINT ( 'NONE', #7685 ) ;
#1086=ORIENTED_EDGE ( 'NONE', *, *, #463, .T. ) ;
#1098=ORIENTED_EDGE ( 'NONE', *, *, #10630, .F. ) ;
#1100=EDGE_CURVE ( 'NONE', #10975, #9875, #12343, .T. ) ;
#1105=CARTESIAN_POINT ( 'NONE',  ( 4.999999999999999112, -9.168210874537443544, -18.05452603534175537 ) ) ;
#1111=ORIENTED_EDGE ( 'NONE', *, *, #4167, .F. ) ;
#1118=FACE_OUTER_BOUND ( 'NONE', #12277, .T. ) ;
#1120=DIRECTION ( 'NONE',  ( 0.000000000000000000, 0.9238795325112877377, -0.3826834323650873393 ) ) ;
#1123=DIRECTION ( 'NONE',  ( 0.000000000000000000, 0.000000000000000000, -1.000000000000000000 ) ) ;
#1132=DIRECTION ( 'NONE',  ( 0.000000000000000000, 0.000000000000000000, 1.000000000000000000 ) ) ;
#1139=CARTESIAN_POINT ( 'NONE',  ( 0.000000000000000000, 0.000000000000000000, 0.000000000000000000 ) ) ;
#1153=ORIENTED_EDGE ( 'NONE', *, *, #11492, .F. ) ;
#1163=VERTEX_POINT ( 'NONE', #3116 ) ;
#1168=DIRECTION ( 'NONE',  ( -1.000000000000000000, 0.000000000000000000, -0.000000000000000000 ) ) ;
#1173=AXIS2_PLACEMENT_3D ( 'NONE', #5680, #1799, #5878 ) ;
#1182=CARTESIAN_POINT ( 'NONE',  ( 0.000000000000000000, 0.000000000000000000, 0.000000000000000000 ) ) ;
#1185=AXIS2_PLACEMENT_3D ( 'NONE', #8772, #199, #4012 ) ;
#1187=AXIS2_PLACEMENT_3D ( 'NONE', #11842, #11660, #469 ) ;
#1189=CARTESIAN_POINT ( 'NONE',  ( 2.499999999999999556, -22.05152472667118957, -15.57980286237495804 ) ) ;
#1192=DIRECTION ( 'NONE',  ( 0.000000000000000000, 0.000000000000000000, 1.000000000000000000 ) ) ;
#1193=DIRECTION ( 'NONE',  ( 0.000000000000000000, -0.9238795325112906243, 0.3826834323650805114 ) ) ;
#1195=AXIS2_PLACEMENT_3D ( 'NONE', #8343, #2710, #12206 ) ;
#1200=ORIENTED_EDGE ( 'NONE', *, *, #8303, .F. ) ;
#1203=CARTESIAN_POINT ( 'NONE',  ( 0.000000000000000000, 0.000000000000000000, 0.000000000000000000 ) ) ;
#1204=VECTOR ( 'NONE', #3845, 1000.000000000000000 ) ;
#1229=CARTESIAN_POINT ( 'NONE',  ( 0.000000000000000000, 0.000000000000000000, 0.000000000000000000 ) ) ;
#1235=AXIS2_PLACEMENT_3D ( 'NONE', #1969, #9596, #149 ) ;
#1240=DIRECTION ( 'NONE',  ( -1.000000000000000000, 0.000000000000000000, 0.000000000000000000 ) ) ;
#1241=AXIS2_PLACEMENT_3D ( 'NONE', #12123, #2513, #753 ) ;
#1246=DIRECTION ( 'NONE',  ( 0.000000000000000000, -1.000000000000000000, -1.048062100068272767E-14 ) ) ;
#1252=CYLINDRICAL_SURFACE ( 'NONE', #5385, 9.600000000009600853 ) ;
#1254=AXIS2_PLACEMENT_3D ( 'NONE', #5188, #4076, #9021 ) ;
#1255=CIRCLE ( 'NONE', #7259, 27.00000000002699707 ) ;
#1257=CIRCLE ( 'NONE', #10644, 20.24900000002024925 ) ;
#1259=LINE ( 'NONE', #5126, #11190 ) ;
#1266=CARTESIAN_POINT ( 'NONE',  ( 0.000000000000000000, 0.000000000000000000, 5.000000000000000000 ) ) ;
#1278=CARTESIAN_POINT ( 'NONE',  ( 4.999999999999999112, 17.79862902732283914, -13.85025647830039119 ) ) ;
#1282=CIRCLE ( 'NONE', #5483, 27.00000000002699707 ) ;
#1286=FACE_OUTER_BOUND ( 'NONE', #2294, .T. ) ;
#1295=ORIENTED_EDGE ( 'NONE', *, *, #9386, .F. ) ;
#1296=ADVANCED_FACE ( 'NONE', ( #8876 ), #8059, .T. ) ;
#1303=CARTESIAN_POINT ( 'NONE',  ( 0.000000000000000000, 0.000000000000000000, 0.000000000000000000 ) ) ;
#1305=VERTEX_POINT ( 'NONE', #11844 ) ;
#1308=ORIENTED_EDGE ( 'NONE', *, *, #4840, .T. ) ;
#1316=ORIENTED_EDGE ( 'NONE', *, *, #2888, .F. ) ;
#1322=ORIENTED_EDGE ( 'NONE', *, *, #9322, .T. ) ;
#1326=EDGE_CURVE ( 'NONE', #4084, #5310, #9616, .T. ) ;
#1334=CARTESIAN_POINT ( 'NONE',  ( 4.999999999999999112, 0.000000000000000000, 20.24900000002024569 ) ) ;
#1336=ORIENTED_EDGE ( 'NONE', *, *, #10129, .T. ) ;
#1343=ADVANCED_FACE ( 'NONE', ( #5477 ), #10276, .T. ) ;
#1346=ADVANCED_FACE ( 'NONE', ( #7351 ), #7413, .T. ) ;
#1352=CARTESIAN_POINT ( 'NONE',  ( 50.00005079999999680, 0.000000000000000000, 0.000000000000000000 ) ) ;
#1354=EDGE_CURVE ( 'NONE', #6904, #11926, #7299, .T. ) ;
#1359=CYLINDRICAL_SURFACE ( 'NONE', #8438, 9.600000000009600853 ) ;
#1361=FACE_OUTER_BOUND ( 'NONE', #8791, .T. ) ;
#1367=EDGE_CURVE ( 'NONE', #644, #4373, #5215, .T. ) ;
#1372=ORIENTED_EDGE ( 'NONE', *, *, #965, .T. ) ;
#1376=AXIS2_PLACEMENT_3D ( 'NONE', #318, #6136, #11817 ) ;
#1385=DIRECTION ( 'NONE',  ( -1.000000000000000000, 0.000000000000000000, -0.000000000000000000 ) ) ;
#1387=CIRCLE ( 'NONE', #2782, 20.24900000002024925 ) ;
#1388=CIRCLE ( 'NONE', #2388, 20.24900000002024925 ) ;
#1393=ORIENTED_EDGE ( 'NONE', *, *, #1585, .T. ) ;
#1399=EDGE_CURVE ( 'NONE', #7808, #11273, #6221, .T. ) ;
#1401=LINE ( 'NONE', #5222, #8999 ) ;
#1403=DIRECTION ( 'NONE',  ( 1.000000000000000000, 0.000000000000000000, 0.000000000000000000 ) ) ;
#1405=AXIS2_PLACEMENT_3D ( 'NONE', #5087, #325, #9907 ) ;
#1408=DIRECTION ( 'NONE',  ( 0.000000000000000000, 0.000000000000000000, 1.000000000000000000 ) ) ;
#1413=DIRECTION ( 'NONE',  ( 0.000000000000000000, 0.000000000000000000, -1.000000000000000000 ) ) ;
#1420=EDGE_CURVE ( 'NONE', #3057, #6849, #10157, .T. ) ;
#1446=CARTESIAN_POINT ( 'NONE',  ( 4.999999999999999112, 18.05452603534165945, 9.168210874537644273 ) ) ;
#1448=LINE ( 'NONE', #5263, #7664 ) ;
#1449=VERTEX_POINT ( 'NONE', #2770 ) ;
#1456=DIRECTION ( 'NONE',  ( 0.000000000000000000, 0.000000000000000000, 1.000000000000000000 ) ) ;
#1459=AXIS2_PLACEMENT_3D ( 'NONE', #3562, #10932, #9198 ) ;
#1461=LINE ( 'NONE', #2142, #10026 ) ;
#1462=EDGE_CURVE ( 'NONE', #3276, #644, #4904, .T. ) ;
#1464=VECTOR ( 'NONE', #5009, 1000.000000000000000 ) ;
#1466=AXIS2_PLACEMENT_3D ( 'NONE', #11729, #5998, #9819 ) ;
#1477=LINE ( 'NONE', #6107, #6590 ) ;
#1484=ORIENTED_EDGE ( 'NONE', *, *, #6864, .F. ) ;
#1487=ORIENTED_EDGE ( 'NONE', *, *, #1520, .T. ) ;
#1488=CARTESIAN_POINT ( 'NONE',  ( 0.000000000000000000, 13.85025647830057416, 17.79862902732270413 ) ) ;
#1492=FACE_OUTER_BOUND ( 'NONE', #2999, .T. ) ;
#1493=EDGE_CURVE ( 'NONE', #4719, #7642, #3775, .T. ) ;
#1499=ORIENTED_EDGE ( 'NONE', *, *, #4582, .T. ) ;
#1500=CARTESIAN_POINT ( 'NONE',  ( 4.999999999999999112, 9.168210874537576771, 18.05452603534168432 ) ) ;
#1502=AXIS2_PLACEMENT_3D ( 'NONE', #8370, #12162, #3617 ) ;
#1508=ORIENTED_EDGE ( 'NONE', *, *, #7159, .T. ) ;
#1520=EDGE_CURVE ( 'NONE', #8668, #2987, #10467, .T. ) ;
#1528=VERTEX_POINT ( 'NONE', #5660 ) ;
#1537=ORIENTED_EDGE ( 'NONE', *, *, #1354, .F. ) ;
#1540=DIRECTION ( 'NONE',  ( -1.000000000000000000, 0.000000000000000000, 0.000000000000000000 ) ) ;
#1551=CARTESIAN_POINT ( 'NONE',  ( 4.999999999999999112, 0.000000000000000000, 0.000000000000000000 ) ) ;
#1557=CARTESIAN_POINT ( 'NONE',  ( 4.999999999999999112, 0.000000000000000000, 0.000000000000000000 ) ) ;
#1563=DIRECTION ( 'NONE',  ( 1.000000000000000000, -0.000000000000000000, -0.000000000000000000 ) ) ;
#1565=FACE_OUTER_BOUND ( 'NONE', #2774, .T. ) ;
#1575=DIRECTION ( 'NONE',  ( 0.000000000000000000, 0.3826834323650905589, -0.9238795325112864054 ) ) ;
#1578=CIRCLE ( 'NONE', #8578, 20.24900000002024569 ) ;
#1579=ORIENTED_EDGE ( 'NONE', *, *, #3540, .T. ) ;
#1585=EDGE_CURVE ( 'NONE', #11456, #3803, #8168, .T. ) ;
#1591=DIRECTION ( 'NONE',  ( 1.000000000000000000, -0.000000000000000000, -0.000000000000000000 ) ) ;
#1595=AXIS2_PLACEMENT_3D ( 'NONE', #10905, #11037, #5102 ) ;
#1599=EDGE_LOOP ( 'NONE', ( #10743, #9182, #3613, #6472 ) ) ;
#1601=CARTESIAN_POINT ( 'NONE',  ( -10.00000000000000000, 0.000000000000000000, 0.000000000000000000 ) ) ;
#1607=CIRCLE ( 'NONE', #8209, 20.24900000002024925 ) ;
#1613=VECTOR ( 'NONE', #4129, 1000.000000000000000 ) ;
#1618=DIRECTION ( 'NONE',  ( -1.000000000000000000, -0.000000000000000000, -0.000000000000000000 ) ) ;
#1623=CIRCLE ( 'NONE', #237, 9.600000000009600853 ) ;
#1625=DIRECTION ( 'NONE',  ( -1.000000000000000000, -0.000000000000000000, 0.000000000000000000 ) ) ;
#1635=ORIENTED_EDGE ( 'NONE', *, *, #10594, .F. ) ;
#1643=PRODUCT_DEFINITION_FORMATION_WITH_SPECIFIED_SOURCE ( 'ANY', '', #6628, .NOT_KNOWN. ) ;
#1644=DIRECTION ( 'NONE',  ( -1.000000000000000000, 0.000000000000000000, -0.000000000000000000 ) ) ;
#1646=CIRCLE ( 'NONE', #2240, 27.00000000002699707 ) ;
#1653=EDGE_LOOP ( 'NONE', ( #6606, #6052, #8075, #4915 ) ) ;
#1654=DIRECTION ( 'NONE',  ( -1.000000000000000000, 0.000000000000000000, 0.000000000000000000 ) ) ;
#1668=AXIS2_PLACEMENT_3D ( 'NONE', #9549, #10605, #5045 ) ;
#1669=ORIENTED_EDGE ( 'NONE', *, *, #7107, .T. ) ;
#1672=EDGE_LOOP ( 'NONE', ( #2756, #9918, #9368, #11098 ) ) ;
#1675=ORIENTED_EDGE ( 'NONE', *, *, #11177, .F. ) ;
#1676=DIRECTION ( 'NONE',  ( -1.000000000000000000, -0.000000000000000000, -0.000000000000000000 ) ) ;
#1687=CARTESIAN_POINT ( 'NONE',  ( 4.999999999999999112, -11.14352537685160982, -19.60720892790264713 ) ) ;
#1691=ORIENTED_EDGE ( 'NONE', *, *, #9470, .F. ) ;
#1699=VECTOR ( 'NONE', #6648, 1000.000000000000000 ) ;
#1702=ADVANCED_FACE ( 'NONE', ( #9959 ), #2144, .T. ) ;
#1705=DIRECTION ( 'NONE',  ( 0.000000000000000000, 0.000000000000000000, -1.000000000000000000 ) ) ;
#1707=DIRECTION ( 'NONE',  ( -1.000000000000000000, -0.000000000000000000, -0.000000000000000000 ) ) ;
#1710=FACE_OUTER_BOUND ( 'NONE', #4150, .T. ) ;
#1715=CARTESIAN_POINT ( 'NONE',  ( 4.999999999999999112, 0.000000000000000000, 0.000000000000000000 ) ) ;
#1718=CARTESIAN_POINT ( 'NONE',  ( 4.999999999999999112, 0.000000000000000000, 0.000000000000000000 ) ) ;
#1722=CARTESIAN_POINT ( 'NONE',  ( 5.000000000000000000, 0.000000000000000000, -1.500000000000000000 ) ) ;
#1726=EDGE_LOOP ( 'NONE', ( #10003, #12274, #2963, #3549 ) ) ;
#1728=DIRECTION ( 'NONE',  ( -1.000000000000000000, -0.000000000000000000, 0.000000000000000000 ) ) ;
#1732=EDGE_CURVE ( 'NONE', #102, #6266, #4956, .T. ) ;
#1733=LINE ( 'NONE', #784, #11796 ) ;
#1735=ORIENTED_EDGE ( 'NONE', *, *, #2971, .F. ) ;
#1737=ORIENTED_EDGE ( 'NONE', *, *, #1743, .T. ) ;
#1738=SURFACE_SIDE_STYLE ('',( #12351 ) ) ;
#1740=VERTEX_POINT ( 'NONE', #11760 ) ;
#1743=EDGE_CURVE ( 'NONE', #1449, #10919, #11133, .T. ) ;
#1746=CYLINDRICAL_SURFACE ( 'NONE', #3847, 9.600000000009600853 ) ;
#1751=DIRECTION ( 'NONE',  ( 0.000000000000000000, 0.000000000000000000, 1.000000000000000000 ) ) ;
#1755=EDGE_CURVE ( 'NONE', #5016, #11122, #5367, .T. ) ;
#1760=CARTESIAN_POINT ( 'NONE',  ( 4.999999999999999112, 0.000000000000000000, 0.000000000000000000 ) ) ;
#1762=FACE_OUTER_BOUND ( 'NONE', #6972, .T. ) ;
#1768=CIRCLE ( 'NONE', #5365, 27.00000000002699707 ) ;
#1769=ORIENTED_EDGE ( 'NONE', *, *, #3924, .F. ) ;
#1772=AXIS2_PLACEMENT_3D ( 'NONE', #9424, #7610, #9546 ) ;
#1775=AXIS2_PLACEMENT_3D ( 'NONE', #7553, #2870, #788 ) ;
#1778=ORIENTED_EDGE ( 'NONE', *, *, #1100, .F. ) ;
#1779=ORIENTED_EDGE ( 'NONE', *, *, #6986, .T. ) ;
#1780=CARTESIAN_POINT ( 'NONE',  ( 4.999999999999999112, 0.000000000000000000, 0.000000000000000000 ) ) ;
#1781=ORIENTED_EDGE ( 'NONE', *, *, #11638, .F. ) ;
#1782=CARTESIAN_POINT ( 'NONE',  ( 4.999999999999999112, -21.74405275335762155, 5.984728032764886407 ) ) ;
#1794=CARTESIAN_POINT ( 'NONE',  ( 4.999999999999999112, -21.74405275335762155, 5.984728032764886407 ) ) ;
#1798=VERTEX_POINT ( 'NONE', #5516 ) ;
#1799=DIRECTION ( 'NONE',  ( -1.000000000000000000, 0.000000000000000000, 0.000000000000000000 ) ) ;
#1803=EDGE_CURVE ( 'NONE', #6404, #10919, #8358, .T. ) ;
#1805=ORIENTED_EDGE ( 'NONE', *, *, #11513, .T. ) ;
#1809=DIRECTION ( 'NONE',  ( -1.000000000000000000, 0.000000000000000000, -0.000000000000000000 ) ) ;
#1811=MECHANICAL_DESIGN_GEOMETRIC_PRESENTATION_REPRESENTATION('',(#11968),#9212);
#1815=AXIS2_PLACEMENT_3D ( 'NONE', #1894, #9519, #942 ) ;
#1819=VERTEX_POINT ( 'NONE', #12069 ) ;
#1824=VECTOR ( 'NONE', #5652, 1000.000000000000000 ) ;
#1827=DIRECTION ( 'NONE',  ( -1.000000000000000000, -0.000000000000000000, -0.000000000000000000 ) ) ;
#1830=DIRECTION ( 'NONE',  ( 0.000000000000000000, 0.000000000000000000, 1.000000000000000000 ) ) ;
#1833=CARTESIAN_POINT ( 'NONE',  ( 0.000000000000000000, 26.33508479058320617, 5.955107813822601237 ) ) ;
#1837=AXIS2_PLACEMENT_3D ( 'NONE', #8345, #7481, #5662 ) ;
#1841=AXIS2_PLACEMENT_3D ( 'NONE', #1030, #7535, #2962 ) ;
#1846=AXIS2_PLACEMENT_3D ( 'NONE', #515, #3157, #2458 ) ;
#1849=CARTESIAN_POINT ( 'NONE',  ( 2.500000000000000444, -22.83261415639512393, 14.41081992069302053 ) ) ;
#1850=VECTOR ( 'NONE', #10513, 1000.000000000000000 ) ;
#1853=ORIENTED_EDGE ( 'NONE', *, *, #1803, .T. ) ;
#1857=VERTEX_POINT ( 'NONE', #9153 ) ;
#1871=CIRCLE ( 'NONE', #1466, 9.600000000009600853 ) ;
#1882=DIRECTION ( 'NONE',  ( 1.000000000000000000, 0.000000000000000000, -0.000000000000000000 ) ) ;
#1884=ORIENTED_EDGE ( 'NONE', *, *, #6691, .F. ) ;
#1889=LINE ( 'NONE', #810, #1699 ) ;
#1894=CARTESIAN_POINT ( 'NONE',  ( -10.00000000000000000, 0.000000000000000000, 0.000000000000000000 ) ) ;
#1900=DIRECTION ( 'NONE',  ( 0.000000000000000000, 0.7071067811865486830, -0.7071067811865464625 ) ) ;
#1902=ORIENTED_EDGE ( 'NONE', *, *, #8213, .F. ) ;
#1913=DIRECTION ( 'NONE',  ( 0.000000000000000000, 0.9238795325112850731, 0.3826834323650938896 ) ) ;
#1914=CARTESIAN_POINT ( 'NONE',  ( 4.999999999999999112, -5.984728032765115557, 21.74405275335756116 ) ) ;
#1915=ORIENTED_EDGE ( 'NONE', *, *, #5846, .F. ) ;
#1922=ORIENTED_EDGE ( 'NONE', *, *, #6247, .T. ) ;
#1928=FACE_OUTER_BOUND ( 'NONE', #6323, .T. ) ;
#1933=LINE ( 'NONE', #11297, #7377 ) ;
#1945=DIRECTION ( 'NONE',  ( -1.000000000000000000, -0.000000000000000000, -0.000000000000000000 ) ) ;
#1948=EDGE_LOOP ( 'NONE', ( #2361, #5191, #7, #1484 ) ) ;
#1954=DIRECTION ( 'NONE',  ( 0.000000000000000000, -1.000000000000000000, -1.048062100068272767E-14 ) ) ;
#1957=CARTESIAN_POINT ( 'NONE',  ( 4.999999999999999112, 13.85025647830057416, 17.79862902732270413 ) ) ;
#1959=ORIENTED_EDGE ( 'NONE', *, *, #1354, .T. ) ;
#1969=CARTESIAN_POINT ( 'NONE',  ( 4.999999999999997335, 0.000000000000000000, 0.000000000000000000 ) ) ;
#1976=CARTESIAN_POINT ( 'NONE',  ( 2.500000000000000444, 26.33508479058329499, -5.955107813822217544 ) ) ;
#1978=ORIENTED_EDGE ( 'NONE', *, *, #9201, .T. ) ;
#1979=AXIS2_PLACEMENT_3D ( 'NONE', #6752, #1062, #11302 ) ;
#1981=VERTEX_POINT ( 'NONE', #11261 ) ;
#1982=ORIENTED_EDGE ( 'NONE', *, *, #4773, .T. ) ;
#1986=CARTESIAN_POINT ( 'NONE',  ( 4.999999999999999112, 21.74405275335758247, 5.984728032765037398 ) ) ;
#1989=ORIENTED_EDGE ( 'NONE', *, *, #8647, .T. ) ;
#2003=EDGE_LOOP ( 'NONE', ( #4948, #9737, #3646, #8879 ) ) ;
#2007=AXIS2_PLACEMENT_3D ( 'NONE', #838, #4402, #7531 ) ;
#2009=ORIENTED_EDGE ( 'NONE', *, *, #8027, .T. ) ;
#2014=ADVANCED_FACE ( 'NONE', ( #4702 ), #10454, .T. ) ;
#2021=DIRECTION ( 'NONE',  ( -1.000000000000000000, 0.000000000000000000, 0.000000000000000000 ) ) ;
#2049=VERTEX_POINT ( 'NONE', #9714 ) ;
#2052=DIRECTION ( 'NONE',  ( -1.000000000000000000, -0.000000000000000000, -0.000000000000000000 ) ) ;
#2058=AXIS2_PLACEMENT_3D ( 'NONE', #10015, #4559, #6321 ) ;
#2061=VERTEX_POINT ( 'NONE', #2310 ) ;
#2063=VECTOR ( 'NONE', #262, 1000.000000000000000 ) ;
#2066=CIRCLE ( 'NONE', #9659, 9.600000000009600853 ) ;
#2072=CARTESIAN_POINT ( 'NONE',  ( 4.999999999999999112, -20.18872947935930284, -1.561154383803435408 ) ) ;
#2078=DIRECTION ( 'NONE',  ( -1.000000000000000000, 0.000000000000000000, 0.000000000000000000 ) ) ;
#2087=CARTESIAN_POINT ( 'NONE',  ( 0.000000000000000000, 1.561154383803505796, -20.18872947935929574 ) ) ;
#2098=CARTESIAN_POINT ( 'NONE',  ( 0.000000000000000000, -13.85025647830044271, -17.79862902732279650 ) ) ;
#2100=EDGE_CURVE ( 'NONE', #1305, #9964, #11742, .T. ) ;
#2110=CARTESIAN_POINT ( 'NONE',  ( 4.999999999999999112, 0.000000000000000000, 0.000000000000000000 ) ) ;
#2111=ORIENTED_EDGE ( 'NONE', *, *, #2100, .F. ) ;
#2118=EDGE_CURVE ( 'NONE', #10544, #12146, #1607, .T. ) ;
#2121=CARTESIAN_POINT ( 'NONE',  ( 4.999999999999999112, -15.37949036966221072, 13.17168466712922914 ) ) ;
#2124=CARTESIAN_POINT ( 'NONE',  ( 4.999999999999999112, 26.60936692326690434, 4.576198416197341245 ) ) ;
#2133=DIRECTION ( 'NONE',  ( -1.000000000000000000, 0.000000000000000000, 0.000000000000000000 ) ) ;
#2134=CARTESIAN_POINT ( 'NONE',  ( 0.000000000000000000, -17.79862902732255137, -13.85025647830076245 ) ) ;
#2142=CARTESIAN_POINT ( 'NONE',  ( 2.499999999999999556, -4.576198416197437169, 26.60936692326689013 ) ) ;
#2144=CYLINDRICAL_SURFACE ( 'NONE', #7764, 27.00000000002699707 ) ;
#2146=DIRECTION ( 'NONE',  ( 0.000000000000000000, 0.7071067811865437980, 0.7071067811865512365 ) ) ;
#2154=DIRECTION ( 'NONE',  ( -1.000000000000000000, 0.000000000000000000, 0.000000000000000000 ) ) ;
#2158=EDGE_CURVE ( 'NONE', #3672, #11750, #3144, .T. ) ;
#2161=ADVANCED_FACE ( 'NONE', ( #7013 ), #8018, .T. ) ;
#2162=ORIENTED_EDGE ( 'NONE', *, *, #8767, .T. ) ;
#2188=AXIS2_PLACEMENT_3D ( 'NONE', #1551, #10178, #8372 ) ;
#2192=LINE ( 'NONE', #3272, #1464 ) ;
#2194=AXIS2_PLACEMENT_3D ( 'NONE', #9870, #11896, #6048 ) ;
#2205=FACE_OUTER_BOUND ( 'NONE', #6021, .T. ) ;
#2210=CARTESIAN_POINT ( 'NONE',  ( 0.000000000000000000, -6.283573709965167176, -19.24938187143303026 ) ) ;
#2215=AXIS2_PLACEMENT_3D ( 'NONE', #6745, #11531, #7803 ) ;
#2216=VERTEX_POINT ( 'NONE', #1446 ) ;
#2219=AXIS2_PLACEMENT_3D ( 'NONE', #3119, #2052, #8877 ) ;
#2221=VECTOR ( 'NONE', #6215, 1000.000000000000000 ) ;
#2224=CIRCLE ( 'NONE', #7030, 20.24900000002024569 ) ;
#2225=AXIS2_PLACEMENT_3D ( 'NONE', #6171, #1540, #597 ) ;
#2229=ORIENTED_EDGE ( 'NONE', *, *, #6864, .T. ) ;
#2236=AXIS2_PLACEMENT_3D ( 'NONE', #1278, #5090, #9155 ) ;
#2240=AXIS2_PLACEMENT_3D ( 'NONE', #640, #7521, #6397 ) ;
#2244=CARTESIAN_POINT ( 'NONE',  ( 4.999999999999999112, 13.85025647830057416, 17.79862902732270413 ) ) ;
#2256=ADVANCED_FACE ( 'NONE', ( #3737 ), #2792, .T. ) ;
#2263=EDGE_LOOP ( 'NONE', ( #11401, #7942, #5233, #986 ) ) ;
#2265=CIRCLE ( 'NONE', #5457, 27.00000000002699707 ) ;
#2271=CYLINDRICAL_SURFACE ( 'NONE', #11210, 20.24900000002024569 ) ;
#2272=EDGE_CURVE ( 'NONE', #1981, #4621, #6263, .T. ) ;
#2274=ADVANCED_FACE ( 'NONE', ( #7272 ), #10076, .T. ) ;
#2276=CARTESIAN_POINT ( 'NONE',  ( 4.999999999999999112, -14.41081992069292994, -22.83261415639518432 ) ) ;
#2277=DIRECTION ( 'NONE',  ( -1.000000000000000000, 0.000000000000000000, -0.000000000000000000 ) ) ;
#2285=DIRECTION ( 'NONE',  ( 0.000000000000000000, 0.7071067811865486830, -0.7071067811865464625 ) ) ;
#2292=CARTESIAN_POINT ( 'NONE',  ( 4.999999999999999112, 13.17168466712928598, 15.37949036966216632 ) ) ;
#2294=EDGE_LOOP ( 'NONE', ( #10801, #5806, #7018, #9755 ) ) ;
#2304=CYLINDRICAL_SURFACE ( 'NONE', #8108, 20.24900000002024569 ) ;
#2310=CARTESIAN_POINT ( 'NONE',  ( 4.999999999999999112, 26.33508479058329499, -5.955107813822219320 ) ) ;
#2328=VERTEX_POINT ( 'NONE', #7876 ) ;
#2329=EDGE_CURVE ( 'NONE', #1083, #10418, #1020, .T. ) ;
#2335=ORIENTED_EDGE ( 'NONE', *, *, #1399, .T. ) ;
#2336=ADVANCED_FACE ( 'NONE', ( #4865 ), #9687, .T. ) ;
#2355=DIRECTION ( 'NONE',  ( -1.000000000000000000, 0.000000000000000000, 0.000000000000000000 ) ) ;
#2356=AXIS2_PLACEMENT_3D ( 'NONE', #8746, #11787, #11722 ) ;
#2357=ORIENTED_EDGE ( 'NONE', *, *, #6887, .T. ) ;
#2359=VECTOR ( 'NONE', #2908, 1000.000000000000000 ) ;
#2361=ORIENTED_EDGE ( 'NONE', *, *, #8783, .F. ) ;
#2363=VECTOR ( 'NONE', #2021, 1000.000000000000000 ) ;
#2369=ORIENTED_EDGE ( 'NONE', *, *, #10422, .T. ) ;
#2370=ORIENTED_EDGE ( 'NONE', *, *, #3102, .F. ) ;
#2371=DIRECTION ( 'NONE',  ( -1.000000000000000000, 0.000000000000000000, 0.000000000000000000 ) ) ;
#2376=CYLINDRICAL_SURFACE ( 'NONE', #4688, 27.00000000002699707 ) ;
#2377=PRODUCT_DEFINITION_CONTEXT ( 'detailed design', #12232, 'design' ) ;
#2388=AXIS2_PLACEMENT_3D ( 'NONE', #6318, #1809, #10126 ) ;
#2390=CARTESIAN_POINT ( 'NONE',  ( 2.499999999999999556, 26.33508479058320617, 5.955107813822601237 ) ) ;
#2391=ORIENTED_EDGE ( 'NONE', *, *, #2517, .T. ) ;
#2397=VECTOR ( 'NONE', #818, 1000.000000000000000 ) ;
#2403=DIRECTION ( 'NONE',  ( 1.000000000000000000, 0.000000000000000000, 0.000000000000000000 ) ) ;
#2408=DIRECTION ( 'NONE',  ( -1.000000000000000000, 0.000000000000000000, 0.000000000000000000 ) ) ;
#2417=CIRCLE ( 'NONE', #224, 27.00000000002699707 ) ;
#2419=CIRCLE ( 'NONE', #2225, 9.600000000009599077 ) ;
#2425=AXIS2_PLACEMENT_3D ( 'NONE', #6803, #4864, #11665 ) ;
#2427=CIRCLE ( 'NONE', #9427, 9.600000000009597301 ) ;
#2431=FACE_OUTER_BOUND ( 'NONE', #8863, .T. ) ;
#2433=EDGE_CURVE ( 'NONE', #7460, #8470, #7618, .T. ) ;
#2434=VECTOR ( 'NONE', #1591, 1000.000000000000000 ) ;
#2437=VECTOR ( 'NONE', #12011, 1000.000000000000000 ) ;
#2447=CIRCLE ( 'NONE', #6658, 20.24900000002024569 ) ;
#2449=DIRECTION ( 'NONE',  ( 0.000000000000000000, 0.000000000000000000, 1.000000000000000000 ) ) ;
#2455=( NAMED_UNIT ( * ) SI_UNIT ( $, .STERADIAN. ) SOLID_ANGLE_UNIT ( ) );
#2458=DIRECTION ( 'NONE',  ( 0.000000000000000000, 0.000000000000000000, 1.000000000000000000 ) ) ;
#2459=DIRECTION ( 'NONE',  ( 0.000000000000000000, 0.000000000000000000, 1.000000000000000000 ) ) ;
#2466=EDGE_LOOP ( 'NONE', ( #4188, #1779, #10162, #1499 ) ) ;
#2469=DIRECTION ( 'NONE',  ( -1.000000000000000000, 0.000000000000000000, 0.000000000000000000 ) ) ;
#2470=CARTESIAN_POINT ( 'NONE',  ( 4.999999999999999112, -22.37914155802287297, 2.791921004064167544 ) ) ;
#2471=FACE_BOUND ( 'NONE', #587, .T. ) ;
#2473=EDGE_LOOP ( 'NONE', ( #759, #11121, #3067, #8261 ) ) ;
#2488=ORIENTED_EDGE ( 'NONE', *, *, #4269, .T. ) ;
#2489=EDGE_CURVE ( 'NONE', #7042, #11456, #5158, .T. ) ;
#2491=DIRECTION ( 'NONE',  ( 0.000000000000000000, 0.000000000000000000, 1.000000000000000000 ) ) ;
#2499=DIRECTION ( 'NONE',  ( 0.000000000000000000, 0.000000000000000000, 1.000000000000000000 ) ) ;
#2501=CYLINDRICAL_SURFACE ( 'NONE', #2058, 20.24900000002024569 ) ;
#2504=DIRECTION ( 'NONE',  ( -1.000000000000000000, 0.000000000000000000, 0.000000000000000000 ) ) ;
#2513=DIRECTION ( 'NONE',  ( 1.000000000000000000, 0.000000000000000000, 0.000000000000000000 ) ) ;
#2517=EDGE_CURVE ( 'NONE', #9474, #644, #610, .T. ) ;
#2524=DIRECTION ( 'NONE',  ( 0.000000000000000000, 0.000000000000000000, 1.000000000000000000 ) ) ;
#2528=EDGE_LOOP ( 'NONE', ( #217, #6881, #10064, #11949 ) ) ;
#2533=CARTESIAN_POINT ( 'NONE',  ( 0.000000000000000000, 0.000000000000000000, 0.000000000000000000 ) ) ;
#2537=EDGE_CURVE ( 'NONE', #978, #1981, #10012, .T. ) ;
#2539=ORIENTED_EDGE ( 'NONE', *, *, #883, .F. ) ;
#2541=ORIENTED_EDGE ( 'NONE', *, *, #3250, .F. ) ;
#2543=ORIENTED_EDGE ( 'NONE', *, *, #2158, .F. ) ;
#2544=CYLINDRICAL_SURFACE ( 'NONE', #9185, 9.600000000009600853 ) ;
#2560=ORIENTED_EDGE ( 'NONE', *, *, #7477, .T. ) ;
#2562=AXIS2_PLACEMENT_3D ( 'NONE', #4360, #8189, #736 ) ;
#2568=DIRECTION ( 'NONE',  ( -1.000000000000000000, 0.000000000000000000, 0.000000000000000000 ) ) ;
#2589=VERTEX_POINT ( 'NONE', #2660 ) ;
#2596=AXIS2_PLACEMENT_3D ( 'NONE', #8360, #1676, #675 ) ;
#2600=DIRECTION ( 'NONE',  ( 0.000000000000000000, 0.7071067811865439090, 0.7071067811865511255 ) ) ;
#2610=ORIENTED_EDGE ( 'NONE', *, *, #4488, .T. ) ;
#2613=EDGE_CURVE ( 'NONE', #10139, #12046, #8237, .T. ) ;
#2618=AXIS2_PLACEMENT_3D ( 'NONE', #5280, #2277, #5144 ) ;
#2622=ORIENTED_EDGE ( 'NONE', *, *, #6922, .T. ) ;
#2627=CARTESIAN_POINT ( 'NONE',  ( 0.000000000000000000, 0.000000000000000000, 0.000000000000000000 ) ) ;
#2632=AXIS2_PLACEMENT_3D ( 'NONE', #2847, #6788, #11577 ) ;
#2634=EDGE_CURVE ( 'NONE', #2216, #6238, #10199, .T. ) ;
#2652=CIRCLE ( 'NONE', #9656, 9.600000000009600853 ) ;
#2654=VECTOR ( 'NONE', #3995, 1000.000000000000000 ) ;
#2660=CARTESIAN_POINT ( 'NONE',  ( 0.000000000000000000, 26.60936692326690789, -4.576198416197345686 ) ) ;
#2664=VERTEX_POINT ( 'NONE', #5413 ) ;
#2667=ADVANCED_FACE ( 'NONE', ( #717 ), #7302, .T. ) ;
#2670=EDGE_CURVE ( 'NONE', #10975, #4084, #1623, .T. ) ;
#2672=CARTESIAN_POINT ( 'NONE',  ( 4.999999999999999112, 13.85025647830082818, -17.79862902732250163 ) ) ;
#2684=FACE_OUTER_BOUND ( 'NONE', #3723, .T. ) ;
#2685=CIRCLE ( 'NONE', #3106, 20.24900000002024569 ) ;
#2692=DIRECTION ( 'NONE',  ( 0.000000000000000000, 0.000000000000000000, 1.000000000000000000 ) ) ;
#2698=EDGE_CURVE ( 'NONE', #9964, #8188, #2427, .T. ) ;
#2700=DIRECTION ( 'NONE',  ( 0.000000000000000000, 0.000000000000000000, 1.000000000000000000 ) ) ;
#2706=ORIENTED_EDGE ( 'NONE', *, *, #4840, .F. ) ;
#2707=CARTESIAN_POINT ( 'NONE',  ( 4.999999999999999112, -5.984728032765115557, 21.74405275335756116 ) ) ;
#2708=ORIENTED_EDGE ( 'NONE', *, *, #9386, .T. ) ;
#2710=DIRECTION ( 'NONE',  ( -1.000000000000000000, 0.000000000000000000, 0.000000000000000000 ) ) ;
#2711=DIRECTION ( 'NONE',  ( 1.000000000000000000, -0.000000000000000000, -0.000000000000000000 ) ) ;
#2720=EDGE_CURVE ( 'NONE', #12254, #2061, #3829, .T. ) ;
#2727=ORIENTED_EDGE ( 'NONE', *, *, #5993, .F. ) ;
#2729=CARTESIAN_POINT ( 'NONE',  ( 0.000000000000000000, -11.14352537685188338, 19.60720892790249081 ) ) ;
#2730=DIRECTION ( 'NONE',  ( 0.000000000000000000, 0.000000000000000000, 1.000000000000000000 ) ) ;
#2745=DIRECTION ( 'NONE',  ( -1.000000000000000000, -0.000000000000000000, 0.000000000000000000 ) ) ;
#2751=LINE ( 'NONE', #6576, #1613 ) ;
#2755=CARTESIAN_POINT ( 'NONE',  ( 4.999999999999999112, -4.576198416197433616, 26.60936692326689013 ) ) ;
#2756=ORIENTED_EDGE ( 'NONE', *, *, #1420, .F. ) ;
#2761=DIRECTION ( 'NONE',  ( 0.000000000000000000, 1.000000000000000000, 3.491481338843133750E-15 ) ) ;
#2769=CARTESIAN_POINT ( 'NONE',  ( 5.000000000000000000, 6.799999999999999822, 0.000000000000000000 ) ) ;
#2770=CARTESIAN_POINT ( 'NONE',  ( 4.999999999999999112, 14.41081992069309869, 22.83261415639507774 ) ) ;
#2774=EDGE_LOOP ( 'NONE', ( #2610, #2967, #2852, #9776 ) ) ;
#2777=ORIENTED_EDGE ( 'NONE', *, *, #8695, .F. ) ;
#2779=VERTEX_POINT ( 'NONE', #3963 ) ;
#2780=AXIS2_PLACEMENT_3D ( 'NONE', #6742, #9613, #8734 ) ;
#2782=AXIS2_PLACEMENT_3D ( 'NONE', #3503, #612, #12052 ) ;
#2783=ADVANCED_FACE ( 'NONE', ( #906, #23 ), #4906, .F. ) ;
#2785=CIRCLE ( 'NONE', #6373, 27.00000000002699707 ) ;
#2786=EDGE_CURVE ( 'NONE', #7042, #11053, #9836, .T. ) ;
#2789=ORIENTED_EDGE ( 'NONE', *, *, #883, .T. ) ;
#2792=CYLINDRICAL_SURFACE ( 'NONE', #4407, 20.24900000002024569 ) ;
#2795=DIRECTION ( 'NONE',  ( 0.000000000000000000, 0.000000000000000000, 1.000000000000000000 ) ) ;
#2798=ORIENTED_EDGE ( 'NONE', *, *, #3294, .F. ) ;
#2800=VERTEX_POINT ( 'NONE', #10526 ) ;
#2806=DIRECTION ( 'NONE',  ( 0.000000000000000000, 0.000000000000000000, 1.000000000000000000 ) ) ;
#2814=AXIS2_PLACEMENT_3D ( 'NONE', #1794, #5495, #2600 ) ;
#2829=CARTESIAN_POINT ( 'NONE',  ( 4.999999999999999112, 22.37914155802285876, 6.808078995945277434 ) ) ;
#2847=CARTESIAN_POINT ( 'NONE',  ( 0.000000000000000000, 19.60720892790252989, -11.14352537685181588 ) ) ;
#2852=ORIENTED_EDGE ( 'NONE', *, *, #10196, .T. ) ;
#2868=ORIENTED_EDGE ( 'NONE', *, *, #9322, .F. ) ;
#2870=DIRECTION ( 'NONE',  ( -1.000000000000000000, -0.000000000000000000, -0.000000000000000000 ) ) ;
#2871=ORIENTED_EDGE ( 'NONE', *, *, #10670, .T. ) ;
#2873=( NAMED_UNIT ( * ) PLANE_ANGLE_UNIT ( ) SI_UNIT ( $, .RADIAN. ) );
#2881=LINE ( 'NONE', #7568, #3459 ) ;
#2883=CARTESIAN_POINT ( 'NONE',  ( 4.999999999999999112, -20.18872947935930284, -1.561154383803435408 ) ) ;
#2888=EDGE_CURVE ( 'NONE', #2328, #6849, #5624, .T. ) ;
#2894=CARTESIAN_POINT ( 'NONE',  ( -10.00000000000000000, 0.000000000000000000, 0.000000000000000000 ) ) ;
#2902=ORIENTED_EDGE ( 'NONE', *, *, #11124, .T. ) ;
#2908=DIRECTION ( 'NONE',  ( -1.000000000000000000, 0.000000000000000000, 0.000000000000000000 ) ) ;
#2909=AXIS2_PLACEMENT_3D ( 'NONE', #10068, #7264, #4357 ) ;
#2919=ORIENTED_EDGE ( 'NONE', *, *, #6845, .T. ) ;
#2921=CYLINDRICAL_SURFACE ( 'NONE', #2780, 27.00000000002699707 ) ;
#2928=SURFACE_STYLE_USAGE ( .BOTH. , #1738 ) ;
#2940=CYLINDRICAL_SURFACE ( 'NONE', #4041, 9.600000000009599077 ) ;
#2945=EDGE_CURVE ( 'NONE', #7805, #12088, #11413, .T. ) ;
#2955=DIRECTION ( 'NONE',  ( 0.000000000000000000, 0.000000000000000000, 1.000000000000000000 ) ) ;
#2961=CARTESIAN_POINT ( 'NONE',  ( 0.000000000000000000, 0.000000000000000000, -1.500000000000000000 ) ) ;
#2962=DIRECTION ( 'NONE',  ( 0.000000000000000000, 0.000000000000000000, 1.000000000000000000 ) ) ;
#2963=ORIENTED_EDGE ( 'NONE', *, *, #9698, .T. ) ;
#2964=ORIENTED_EDGE ( 'NONE', *, *, #2433, .F. ) ;
#2967=ORIENTED_EDGE ( 'NONE', *, *, #7974, .T. ) ;
#2970=ORIENTED_EDGE ( 'NONE', *, *, #3515, .F. ) ;
#2971=EDGE_CURVE ( 'NONE', #5514, #7042, #2224, .T. ) ;
#2976=EDGE_LOOP ( 'NONE', ( #2335, #11911, #8598, #7319 ) ) ;
#2982=DIRECTION ( 'NONE',  ( -1.000000000000000000, -0.000000000000000000, 0.000000000000000000 ) ) ;
#2987=VERTEX_POINT ( 'NONE', #2210 ) ;
#2991=LINE ( 'NONE', #8810, #10752 ) ;
#2993=VECTOR ( 'NONE', #9648, 1000.000000000000000 ) ;
#2998=DIRECTION ( 'NONE',  ( 1.000000000000000000, 0.000000000000000000, 0.000000000000000000 ) ) ;
#2999=EDGE_LOOP ( 'NONE', ( #8771, #2488, #11058, #5707 ) ) ;
#3004=CARTESIAN_POINT ( 'NONE',  ( -10.00000000000000000, 0.000000000000000000, 0.000000000000000000 ) ) ;
#3005=EDGE_CURVE ( 'NONE', #11926, #11497, #1034, .T. ) ;
#3011=CARTESIAN_POINT ( 'NONE',  ( 0.000000000000000000, 0.000000000000000000, 0.000000000000000000 ) ) ;
#3016=ORIENTED_EDGE ( 'NONE', *, *, #3877, .T. ) ;
#3027=VECTOR ( 'NONE', #10207, 1000.000000000000000 ) ;
#3028=AXIS2_PLACEMENT_3D ( 'NONE', #11775, #8985, #10050 ) ;
#3033=CARTESIAN_POINT ( 'NONE',  ( 4.999999999999999112, 2.791921004064247480, 22.37914155802286942 ) ) ;
#3046=ORIENTED_EDGE ( 'NONE', *, *, #6922, .F. ) ;
#3048=( GEOMETRIC_REPRESENTATION_CONTEXT ( 3 ) GLOBAL_UNCERTAINTY_ASSIGNED_CONTEXT ( ( #8161 ) ) GLOBAL_UNIT_ASSIGNED_CONTEXT ( ( #425, #2873, #9440 ) ) REPRESENTATION_CONTEXT ( 'NONE', 'WORKASPACE' ) );
#3052=ORIENTED_EDGE ( 'NONE', *, *, #11051, .T. ) ;
#3057=VERTEX_POINT ( 'NONE', #10948 ) ;
#3058=EDGE_CURVE ( 'NONE', #6875, #7704, #11703, .T. ) ;
#3067=ORIENTED_EDGE ( 'NONE', *, *, #9209, .T. ) ;
#3071=CARTESIAN_POINT ( 'NONE',  ( 0.000000000000000000, -13.85025647830069317, 17.79862902732260110 ) ) ;
#3075=ADVANCED_FACE ( 'NONE', ( #6966 ), #7967, .T. ) ;
#3076=DIRECTION ( 'NONE',  ( 0.000000000000000000, 0.000000000000000000, -1.000000000000000000 ) ) ;
#3077=DIRECTION ( 'NONE',  ( 0.000000000000000000, 0.3826834323650905589, -0.9238795325112864054 ) ) ;
#3089=CARTESIAN_POINT ( 'NONE',  ( 0.000000000000000000, 0.000000000000000000, 0.000000000000000000 ) ) ;
#3091=EDGE_LOOP ( 'NONE', ( #9647, #7151, #8362, #1322 ) ) ;
#3092=CARTESIAN_POINT ( 'NONE',  ( 4.999999999999999112, -26.33508479058324170, 5.955107813822415608 ) ) ;
#3098=AXIS2_PLACEMENT_3D ( 'NONE', #3766, #10579, #4898 ) ;
#3100=DIRECTION ( 'NONE',  ( -1.000000000000000000, 0.000000000000000000, 0.000000000000000000 ) ) ;
#3102=EDGE_CURVE ( 'NONE', #11449, #138, #4644, .T. ) ;
#3103=DIRECTION ( 'NONE',  ( 0.000000000000000000, -1.000000000000000000, 0.000000000000000000 ) ) ;
#3106=AXIS2_PLACEMENT_3D ( 'NONE', #1182, #6832, #5894 ) ;
#3112=ADVANCED_FACE ( 'NONE', ( #4517 ), #9105, .T. ) ;
#3113=CARTESIAN_POINT ( 'NONE',  ( 4.999999999999999112, 0.000000000000000000, 0.000000000000000000 ) ) ;
#3114=ORIENTED_EDGE ( 'NONE', *, *, #5318, .T. ) ;
#3116=CARTESIAN_POINT ( 'NONE',  ( 0.000000000000000000, 21.74405275335758247, 15.58472803277463825 ) ) ;
#3118=EDGE_CURVE ( 'NONE', #6551, #3276, #5437, .T. ) ;
#3119=CARTESIAN_POINT ( 'NONE',  ( 0.000000000000000000, 0.000000000000000000, 0.000000000000000000 ) ) ;
#3123=EDGE_LOOP ( 'NONE', ( #5510, #11696, #8755, #10471 ) ) ;
#3133=CARTESIAN_POINT ( 'NONE',  ( 0.000000000000000000, 11.14352537685202016, -19.60720892790241265 ) ) ;
#3134=EDGE_LOOP ( 'NONE', ( #5458, #4289, #2919, #11400 ) ) ;
#3137=DIRECTION ( 'NONE',  ( -1.000000000000000000, 0.000000000000000000, 0.000000000000000000 ) ) ;
#3138=CARTESIAN_POINT ( 'NONE',  ( 4.999999999999999112, 20.18872947935930995, 1.561154383803294410 ) ) ;
#3142=EDGE_CURVE ( 'NONE', #5656, #10139, #245, .T. ) ;
#3144=LINE ( 'NONE', #1189, #11779 ) ;
#3145=CYLINDRICAL_SURFACE ( 'NONE', #3858, 9.600000000009600853 ) ;
#3153=ORIENTED_EDGE ( 'NONE', *, *, #3058, .F. ) ;
#3155=FACE_OUTER_BOUND ( 'NONE', #4521, .T. ) ;
#3157=DIRECTION ( 'NONE',  ( -1.000000000000000000, -0.000000000000000000, -0.000000000000000000 ) ) ;
#3166=DIRECTION ( 'NONE',  ( 1.000000000000000000, -0.000000000000000000, 0.000000000000000000 ) ) ;
#3169=FACE_OUTER_BOUND ( 'NONE', #165, .T. ) ;
#3178=AXIS2_PLACEMENT_3D ( 'NONE', #8076, #11620, #6065 ) ;
#3181=EDGE_CURVE ( 'NONE', #12228, #7460, #11083, .T. ) ;
#3187=VERTEX_POINT ( 'NONE', #4386 ) ;
#3202=DIRECTION ( 'NONE',  ( -1.000000000000000000, 0.000000000000000000, -0.000000000000000000 ) ) ;
#3206=CYLINDRICAL_SURFACE ( 'NONE', #1185, 20.24900000002024569 ) ;
#3213=ORIENTED_EDGE ( 'NONE', *, *, #9033, .F. ) ;
#3226=AXIS2_PLACEMENT_3D ( 'NONE', #6049, #291, #4105 ) ;
#3230=AXIS2_PLACEMENT_3D ( 'NONE', #10540, #5047, #4794 ) ;
#3237=EDGE_LOOP ( 'NONE', ( #729, #6792, #12079, #12349 ) ) ;
#3239=ORIENTED_EDGE ( 'NONE', *, *, #6313, .F. ) ;
#3245=CIRCLE ( 'NONE', #9639, 9.600000000009599077 ) ;
#3247=AXIS2_PLACEMENT_3D ( 'NONE', #9580, #8711, #7659 ) ;
#3249=DIRECTION ( 'NONE',  ( 0.000000000000000000, 0.000000000000000000, 1.000000000000000000 ) ) ;
#3250=EDGE_CURVE ( 'NONE', #102, #3326, #5640, .T. ) ;
#3255=ORIENTED_EDGE ( 'NONE', *, *, #9698, .F. ) ;
#3258=ORIENTED_EDGE ( 'NONE', *, *, #1462, .F. ) ;
#3261=LINE ( 'NONE', #3138, #7495 ) ;
#3265=AXIS2_PLACEMENT_3D ( 'NONE', #2244, #7818, #3077 ) ;
#3267=EDGE_CURVE ( 'NONE', #8693, #3572, #137, .T. ) ;
#3269=DIRECTION ( 'NONE',  ( -1.000000000000000000, 0.000000000000000000, 0.000000000000000000 ) ) ;
#3272=CARTESIAN_POINT ( 'NONE',  ( 4.999999999999999112, 19.24938187143305512, -6.283573709965099674 ) ) ;
#3276=VERTEX_POINT ( 'NONE', #12256 ) ;
#3281=CARTESIAN_POINT ( 'NONE',  ( 4.999999999999999112, -22.37914155802283034, -2.791921004064479739 ) ) ;
#3286=DIRECTION ( 'NONE',  ( -1.000000000000000000, 0.000000000000000000, 0.000000000000000000 ) ) ;
#3287=DIRECTION ( 'NONE',  ( 0.000000000000000000, 0.000000000000000000, -1.000000000000000000 ) ) ;
#3292=DIRECTION ( 'NONE',  ( 1.000000000000000000, 0.000000000000000000, 0.000000000000000000 ) ) ;
#3294=EDGE_CURVE ( 'NONE', #2779, #4243, #891, .T. ) ;
#3296=EDGE_CURVE ( 'NONE', #7220, #10481, #11427, .T. ) ;
#3301=CARTESIAN_POINT ( 'NONE',  ( 0.000000000000000000, 11.14352537685174660, 19.60720892790256897 ) ) ;
#3311=DIRECTION ( 'NONE',  ( -1.000000000000000000, 0.000000000000000000, 0.000000000000000000 ) ) ;
#3312=ORIENTED_EDGE ( 'NONE', *, *, #3005, .T. ) ;
#3313=CARTESIAN_POINT ( 'NONE',  ( 0.000000000000000000, -19.24938187143300539, 6.283573709965241783 ) ) ;
#3315=CARTESIAN_POINT ( 'NONE',  ( 4.999999999999999112, -17.79862902732275032, 13.85025647830051021 ) ) ;
#3318=ORIENTED_EDGE ( 'NONE', *, *, #8595, .F. ) ;
#3324=DIRECTION ( 'NONE',  ( -1.000000000000000000, 0.000000000000000000, -0.000000000000000000 ) ) ;
#3326=VERTEX_POINT ( 'NONE', #2755 ) ;
#3329=CARTESIAN_POINT ( 'NONE',  ( 0.000000000000000000, 0.000000000000000000, 0.000000000000000000 ) ) ;
#3330=ORIENTED_EDGE ( 'NONE', *, *, #5386, .T. ) ;
#3332=EDGE_CURVE ( 'NONE', #4444, #4464, #4759, .T. ) ;
#3338=DIRECTION ( 'NONE',  ( 0.000000000000000000, -1.000000000000000000, -1.047444401652940007E-14 ) ) ;
#3350=ORIENTED_EDGE ( 'NONE', *, *, #12172, .T. ) ;
#3351=LINE ( 'NONE', #2292, #8646 ) ;
#3360=DIRECTION ( 'NONE',  ( 0.000000000000000000, 0.000000000000000000, 1.000000000000000000 ) ) ;
#3368=CARTESIAN_POINT ( 'NONE',  ( 0.000000000000000000, 0.000000000000000000, 0.000000000000000000 ) ) ;
#3375=DIRECTION ( 'NONE',  ( -1.000000000000000000, -0.000000000000000000, 0.000000000000000000 ) ) ;
#3382=DIRECTION ( 'NONE',  ( -1.000000000000000000, 0.000000000000000000, 0.000000000000000000 ) ) ;
#3383=AXIS2_PLACEMENT_3D ( 'NONE', #3368, #1618, #4497 ) ;
#3387=EDGE_LOOP ( 'NONE', ( #10721, #8540, #10310, #7323 ) ) ;
#3391=AXIS2_PLACEMENT_3D ( 'NONE', #6076, #4128, #9084 ) ;
#3393=CARTESIAN_POINT ( 'NONE',  ( 4.999999999999999112, 1.561154383803221579, 20.18872947935931705 ) ) ;
#3397=DIRECTION ( 'NONE',  ( -1.000000000000000000, -0.000000000000000000, -0.000000000000000000 ) ) ;
#3399=DIRECTION ( 'NONE',  ( 0.000000000000000000, -0.3826834323650971093, 0.9238795325112837409 ) ) ;
#3403=AXIS2_PLACEMENT_3D ( 'NONE', #11542, #10552, #4807 ) ;
#3404=CARTESIAN_POINT ( 'NONE',  ( 4.999999999999999112, -9.168210874537708222, 18.05452603534162748 ) ) ;
#3406=CARTESIAN_POINT ( 'NONE',  ( 4.999999999999999112, -22.37914155802283034, -2.791921004064479739 ) ) ;
#3420=DIRECTION ( 'NONE',  ( -1.000000000000000000, -0.000000000000000000, -0.000000000000000000 ) ) ;
#3427=DIRECTION ( 'NONE',  ( 1.000000000000000000, 0.000000000000000000, 0.000000000000000000 ) ) ;
#3429=ORIENTED_EDGE ( 'NONE', *, *, #11974, .F. ) ;
#3430=DIRECTION ( 'NONE',  ( 0.000000000000000000, -0.9238795325112826307, -0.3826834323650997183 ) ) ;
#3431=CIRCLE ( 'NONE', #2632, 9.600000000009600853 ) ;
#3436=DIRECTION ( 'NONE',  ( 0.000000000000000000, 0.000000000000000000, 1.000000000000000000 ) ) ;
#3439=MECHANICAL_DESIGN_GEOMETRIC_PRESENTATION_REPRESENTATION('',(#639),#7248);
#3457=CARTESIAN_POINT ( 'NONE',  ( 4.999999999999999112, 11.14352537685174660, 19.60720892790256897 ) ) ;
#3459=VECTOR ( 'NONE', #1882, 1000.000000000000000 ) ;
#3470=CARTESIAN_POINT ( 'NONE',  ( 4.999999999999999112, -6.283573709965446064, 19.24938187143294144 ) ) ;
#3472=DIRECTION ( 'NONE',  ( -1.000000000000000000, 0.000000000000000000, 0.000000000000000000 ) ) ;
#3474=ORIENTED_EDGE ( 'NONE', *, *, #5702, .T. ) ;
#3476=EDGE_CURVE ( 'NONE', #11705, #7774, #8839, .T. ) ;
#3478=LINE ( 'NONE', #2769, #3990 ) ;
#3485=ORIENTED_EDGE ( 'NONE', *, *, #746, .T. ) ;
#3489=EDGE_CURVE ( 'NONE', #4720, #4328, #8056, .T. ) ;
#3490=CYLINDRICAL_SURFACE ( 'NONE', #8177, 27.00000000002699707 ) ;
#3492=AXIS2_PLACEMENT_3D ( 'NONE', #11455, #9475, #9526 ) ;
#3501=CARTESIAN_POINT ( 'NONE',  ( 4.999999999999999112, -15.37949036966221072, 13.17168466712922914 ) ) ;
#3502=VERTEX_POINT ( 'NONE', #10827 ) ;
#3503=CARTESIAN_POINT ( 'NONE',  ( 0.000000000000000000, 0.000000000000000000, 0.000000000000000000 ) ) ;
#3506=CARTESIAN_POINT ( 'NONE',  ( -10.00000000000000000, 0.000000000000000000, 0.000000000000000000 ) ) ;
#3511=CARTESIAN_POINT ( 'NONE',  ( 4.999999999999999112, 0.000000000000000000, 0.000000000000000000 ) ) ;
#3512=FACE_OUTER_BOUND ( 'NONE', #11941, .T. ) ;
#3515=EDGE_CURVE ( 'NONE', #9230, #1528, #1257, .T. ) ;
#3517=CARTESIAN_POINT ( 'NONE',  ( 0.000000000000000000, -14.41081992069325857, 22.83261415639497827 ) ) ;
#3520=CARTESIAN_POINT ( 'NONE',  ( 4.999999999999999112, -6.283573709965167176, -19.24938187143303026 ) ) ;
#3530=ORIENTED_EDGE ( 'NONE', *, *, #5182, .T. ) ;
#3535=DIRECTION ( 'NONE',  ( 0.000000000000000000, 0.3826834323650905589, -0.9238795325112864054 ) ) ;
#3537=CARTESIAN_POINT ( 'NONE',  ( -10.00000000000000000, 0.000000000000000000, 0.000000000000000000 ) ) ;
#3540=EDGE_CURVE ( 'NONE', #8258, #1032, #6253, .T. ) ;
#3549=ORIENTED_EDGE ( 'NONE', *, *, #4269, .F. ) ;
#3562=CARTESIAN_POINT ( 'NONE',  ( 4.999999999999999112, 0.000000000000000000, 0.000000000000000000 ) ) ;
#3568=EDGE_CURVE ( 'NONE', #10665, #11306, #11231, .T. ) ;
#3572=VERTEX_POINT ( 'NONE', #8196 ) ;
#3577=DIRECTION ( 'NONE',  ( -1.000000000000000000, 0.000000000000000000, 0.000000000000000000 ) ) ;
#3579=ORIENTED_EDGE ( 'NONE', *, *, #645, .T. ) ;
#3581=CARTESIAN_POINT ( 'NONE',  ( 0.000000000000000000, 13.17168466712950092, -15.37949036966198157 ) ) ;
#3597=CARTESIAN_POINT ( 'NONE',  ( 0.000000000000000000, -15.37949036966221072, 13.17168466712922914 ) ) ;
#3602=CIRCLE ( 'NONE', #6600, 20.24900000002024569 ) ;
#3608=CARTESIAN_POINT ( 'NONE',  ( 4.999999999999999112, -26.60936692326693276, 4.576198416197154728 ) ) ;
#3613=ORIENTED_EDGE ( 'NONE', *, *, #4876, .F. ) ;
#3615=ORIENTED_EDGE ( 'NONE', *, *, #8530, .F. ) ;
#3617=DIRECTION ( 'NONE',  ( 0.000000000000000000, 1.000000000000000000, 3.491481338843133750E-15 ) ) ;
#3621=AXIS2_PLACEMENT_3D ( 'NONE', #2470, #529, #8233 ) ;
#3624=DIRECTION ( 'NONE',  ( 0.000000000000000000, -0.7071067811865389130, -0.7071067811865562325 ) ) ;
#3625=ADVANCED_FACE ( 'NONE', ( #10131 ), #2501, .T. ) ;
#3634=CYLINDRICAL_SURFACE ( 'NONE', #633, 27.00000000002699707 ) ;
#3642=EDGE_CURVE ( 'NONE', #9710, #1032, #1448, .T. ) ;
#3646=ORIENTED_EDGE ( 'NONE', *, *, #8677, .F. ) ;
#3648=DIRECTION ( 'NONE',  ( 0.000000000000000000, -1.000000000000000000, -1.047444401652940007E-14 ) ) ;
#3650=CIRCLE ( 'NONE', #10642, 9.600000000009604406 ) ;
#3652=ORIENTED_EDGE ( 'NONE', *, *, #9761, .F. ) ;
#3663=DIRECTION ( 'NONE',  ( 0.000000000000000000, 0.000000000000000000, 1.000000000000000000 ) ) ;
#3669=ORIENTED_EDGE ( 'NONE', *, *, #2945, .F. ) ;
#3672=VERTEX_POINT ( 'NONE', #7274 ) ;
#3679=AXIS2_PLACEMENT_3D ( 'NONE', #11767, #3292, #6218 ) ;
#3689=CARTESIAN_POINT ( 'NONE',  ( 4.999999999999999112, -15.37949036966202598, -13.17168466712944408 ) ) ;
#3692=DIRECTION ( 'NONE',  ( -1.000000000000000000, 0.000000000000000000, -0.000000000000000000 ) ) ;
#3693=ORIENTED_EDGE ( 'NONE', *, *, #886, .F. ) ;
#3701=CARTESIAN_POINT ( 'NONE',  ( 4.999999999999999112, -22.05152472667140628, 15.57980286237465251 ) ) ;
#3711=DIRECTION ( 'NONE',  ( 0.000000000000000000, 0.000000000000000000, 1.000000000000000000 ) ) ;
#3717=EDGE_CURVE ( 'NONE', #238, #3187, #2881, .T. ) ;
#3721=CARTESIAN_POINT ( 'NONE',  ( 0.000000000000000000, 13.85025647830082818, -17.79862902732250163 ) ) ;
#3723=EDGE_LOOP ( 'NONE', ( #5285, #5130, #462, #7356 ) ) ;
#3728=PRODUCT_CONTEXT ( 'NONE', #7131, 'mechanical' ) ;
#3732=CARTESIAN_POINT ( 'NONE',  ( 0.000000000000000000, 1.561154383803221579, 20.18872947935931705 ) ) ;
#3737=FACE_OUTER_BOUND ( 'NONE', #11421, .T. ) ;
#3738=EDGE_LOOP ( 'NONE', ( #6185, #2964, #10408, #5431 ) ) ;
#3739=EDGE_CURVE ( 'NONE', #4243, #4722, #12025, .T. ) ;
#3742=EDGE_LOOP ( 'NONE', ( #1675, #2009, #1781, #3213 ) ) ;
#3743=LINE ( 'NONE', #5614, #6713 ) ;
#3745=CARTESIAN_POINT ( 'NONE',  ( 50.00005079999999680, 4.769696007084728073, 1.500000000000000000 ) ) ;
#3746=CYLINDRICAL_SURFACE ( 'NONE', #11380, 9.600000000009599077 ) ;
#3747=LINE ( 'NONE', #6704, #10345 ) ;
#3748=CARTESIAN_POINT ( 'NONE',  ( 4.999999999999999112, -5.984728032764810024, -21.74405275335764287 ) ) ;
#3749=ORIENTED_EDGE ( 'NONE', *, *, #10083, .F. ) ;
#3766=CARTESIAN_POINT ( 'NONE',  ( 4.999999999999999112, -2.791921004064099154, -22.37914155802288363 ) ) ;
#3771=EDGE_CURVE ( 'NONE', #6266, #8991, #3861, .T. ) ;
#3774=CARTESIAN_POINT ( 'NONE',  ( 0.000000000000000000, 4.576198416197625463, -26.60936692326685815 ) ) ;
#3775=LINE ( 'NONE', #1849, #5970 ) ;
#3776=ADVANCED_FACE ( 'NONE', ( #10499 ), #1746, .T. ) ;
#3782=ORIENTED_EDGE ( 'NONE', *, *, #10630, .T. ) ;
#3783=CARTESIAN_POINT ( 'NONE',  ( 4.999999999999997335, 4.769696007084728073, 1.500000000000000000 ) ) ;
#3797=CARTESIAN_POINT ( 'NONE',  ( 0.000000000000000000, 0.000000000000000000, 0.000000000000000000 ) ) ;
#3800=ORIENTED_EDGE ( 'NONE', *, *, #7710, .F. ) ;
#3803=VERTEX_POINT ( 'NONE', #6564 ) ;
#3814=DIRECTION ( 'NONE',  ( -1.000000000000000000, 0.000000000000000000, 0.000000000000000000 ) ) ;
#3820=VECTOR ( 'NONE', #10280, 1000.000000000000000 ) ;
#3823=DIRECTION ( 'NONE',  ( -1.000000000000000000, 0.000000000000000000, -0.000000000000000000 ) ) ;
#3829=CIRCLE ( 'NONE', #7638, 27.00000000002699707 ) ;
#3830=CYLINDRICAL_SURFACE ( 'NONE', #800, 9.600000000009600853 ) ;
#3832=DIRECTION ( 'NONE',  ( -1.000000000000000000, -0.000000000000000000, 0.000000000000000000 ) ) ;
#3837=VECTOR ( 'NONE', #3103, 1000.000000000000000 ) ;
#3838=ORIENTED_EDGE ( 'NONE', *, *, #5995, .F. ) ;
#3839=CARTESIAN_POINT ( 'NONE',  ( 4.999999999999999112, -1.561154383803364798, 20.18872947935930640 ) ) ;
#3845=DIRECTION ( 'NONE',  ( -1.000000000000000000, 0.000000000000000000, 0.000000000000000000 ) ) ;
#3847=AXIS2_PLACEMENT_3D ( 'NONE', #3748, #7450, #10440 ) ;
#3851=ORIENTED_EDGE ( 'NONE', *, *, #9665, .T. ) ;
#3854=CARTESIAN_POINT ( 'NONE',  ( 4.999999999999999112, 22.05152472667151642, -15.57980286237449619 ) ) ;
#3858=AXIS2_PLACEMENT_3D ( 'NONE', #9769, #10826, #7135 ) ;
#3861=CIRCLE ( 'NONE', #8259, 27.00000000002699707 ) ;
#3866=DIRECTION ( 'NONE',  ( -1.000000000000000000, 0.000000000000000000, 0.000000000000000000 ) ) ;
#3870=DIRECTION ( 'NONE',  ( -1.000000000000000000, -0.000000000000000000, 0.000000000000000000 ) ) ;
#3875=VERTEX_POINT ( 'NONE', #9883 ) ;
#3877=EDGE_CURVE ( 'NONE', #5016, #8451, #7268, .T. ) ;
#3894=AXIS2_PLACEMENT_3D ( 'NONE', #2707, #3472, #8160 ) ;
#3902=EDGE_CURVE ( 'NONE', #7155, #7438, #1871, .T. ) ;
#3904=DIRECTION ( 'NONE',  ( -1.000000000000000000, 0.000000000000000000, 0.000000000000000000 ) ) ;
#3907=VERTEX_POINT ( 'NONE', #6823 ) ;
#3915=DIRECTION ( 'NONE',  ( -1.000000000000000000, -0.000000000000000000, -0.000000000000000000 ) ) ;
#3918=ORIENTED_EDGE ( 'NONE', *, *, #8027, .F. ) ;
#3924=EDGE_CURVE ( 'NONE', #3502, #4444, #2066, .T. ) ;
#3925=ORIENTED_EDGE ( 'NONE', *, *, #10118, .F. ) ;
#3926=CYLINDRICAL_SURFACE ( 'NONE', #12149, 9.600000000009600853 ) ;
#3933=EDGE_CURVE ( 'NONE', #486, #3875, #8457, .T. ) ;
#3943=DIRECTION ( 'NONE',  ( -1.000000000000000000, 0.000000000000000000, 0.000000000000000000 ) ) ;
#3947=EDGE_CURVE ( 'NONE', #6352, #10042, #6890, .T. ) ;
#3948=EDGE_CURVE ( 'NONE', #11306, #2216, #7669, .T. ) ;
#3953=CARTESIAN_POINT ( 'NONE',  ( 0.000000000000000000, 6.283573709965309284, 19.24938187143298052 ) ) ;
#3960=FACE_OUTER_BOUND ( 'NONE', #12326, .T. ) ;
#3961=CARTESIAN_POINT ( 'NONE',  ( 4.999999999999999112, -6.283573709965167176, -19.24938187143303026 ) ) ;
#3963=CARTESIAN_POINT ( 'NONE',  ( 0.000000000000000000, 5.955107813822504426, 26.33508479058322749 ) ) ;
#3976=DIRECTION ( 'NONE',  ( 0.000000000000000000, -0.3826834323650773473, -0.9238795325112918455 ) ) ;
#3977=CARTESIAN_POINT ( 'NONE',  ( 0.000000000000000000, -15.37949036966202598, -13.17168466712944408 ) ) ;
#3981=DIRECTION ( 'NONE',  ( -1.000000000000000000, -0.000000000000000000, -0.000000000000000000 ) ) ;
#3985=VERTEX_POINT ( 'NONE', #10936 ) ;
#3989=DIRECTION ( 'NONE',  ( 0.000000000000000000, 0.3826834323650905589, -0.9238795325112864054 ) ) ;
#3990=VECTOR ( 'NONE', #2524, 1000.000000000000000 ) ;
#3994=CARTESIAN_POINT ( 'NONE',  ( 4.999999999999999112, 21.74405275335766419, -5.984728032764733641 ) ) ;
#3995=DIRECTION ( 'NONE',  ( 1.000000000000000000, -0.000000000000000000, -0.000000000000000000 ) ) ;
#3999=EDGE_CURVE ( 'NONE', #8668, #8041, #5259, .T. ) ;
#4003=EDGE_CURVE ( 'NONE', #2987, #8258, #5060, .T. ) ;
#4012=DIRECTION ( 'NONE',  ( 0.000000000000000000, 0.000000000000000000, 1.000000000000000000 ) ) ;
#4013=DIRECTION ( 'NONE',  ( -1.000000000000000000, -0.000000000000000000, -0.000000000000000000 ) ) ;
#4024=AXIS2_PLACEMENT_3D ( 'NONE', #2533, #537, #4346 ) ;
#4026=DIRECTION ( 'NONE',  ( -1.000000000000000000, 0.000000000000000000, -0.000000000000000000 ) ) ;
#4034=AXIS2_PLACEMENT_3D ( 'NONE', #11095, #5349, #9241 ) ;
#4035=DIRECTION ( 'NONE',  ( 0.000000000000000000, 0.000000000000000000, 1.000000000000000000 ) ) ;
#4036=VECTOR ( 'NONE', #9333, 1000.000000000000000 ) ;
#4041=AXIS2_PLACEMENT_3D ( 'NONE', #937, #6758, #4883 ) ;
#4043=CYLINDRICAL_SURFACE ( 'NONE', #1187, 9.600000000009600853 ) ;
#4045=CYLINDRICAL_SURFACE ( 'NONE', #1001, 9.600000000009600853 ) ;
#4062=AXIS2_PLACEMENT_3D ( 'NONE', #3133, #10803, #10742 ) ;
#4076=DIRECTION ( 'NONE',  ( 1.000000000000000000, 0.000000000000000000, 0.000000000000000000 ) ) ;
#4084=VERTEX_POINT ( 'NONE', #5193 ) ;
#4085=DIRECTION ( 'NONE',  ( -1.000000000000000000, 0.000000000000000000, -0.000000000000000000 ) ) ;
#4105=DIRECTION ( 'NONE',  ( -1.000000000000000000, 0.000000000000000000, -0.000000000000000000 ) ) ;
#4115=DIRECTION ( 'NONE',  ( -1.000000000000000000, 0.000000000000000000, 0.000000000000000000 ) ) ;
#4128=DIRECTION ( 'NONE',  ( -1.000000000000000000, 0.000000000000000000, 0.000000000000000000 ) ) ;
#4129=DIRECTION ( 'NONE',  ( -0.000000000000000000, 1.000000000000000000, 0.000000000000000000 ) ) ;
#4131=CARTESIAN_POINT ( 'NONE',  ( 4.999999999999999112, 19.60720892790252989, -11.14352537685181588 ) ) ;
#4133=ORIENTED_EDGE ( 'NONE', *, *, #6071, .T. ) ;
#4134=ORIENTED_EDGE ( 'NONE', *, *, #2537, .T. ) ;
#4140=FACE_OUTER_BOUND ( 'NONE', #8271, .T. ) ;
#4141=DIRECTION ( 'NONE',  ( -1.000000000000000000, 0.000000000000000000, 0.000000000000000000 ) ) ;
#4143=CARTESIAN_POINT ( 'NONE',  ( 4.999999999999999112, 0.000000000000000000, 0.000000000000000000 ) ) ;
#4148=EDGE_CURVE ( 'NONE', #536, #486, #2265, .T. ) ;
#4150=EDGE_LOOP ( 'NONE', ( #11581, #6039, #1111, #2708 ) ) ;
#4161=CIRCLE ( 'NONE', #970, 9.600000000009602630 ) ;
#4163=AXIS2_PLACEMENT_3D ( 'NONE', #306, #246, #3076 ) ;
#4167=EDGE_CURVE ( 'NONE', #8321, #12146, #4749, .T. ) ;
#4170=AXIS2_PLACEMENT_3D ( 'NONE', #2672, #1728, #11338 ) ;
#4173=DIRECTION ( 'NONE',  ( 0.000000000000000000, 0.000000000000000000, 1.000000000000000000 ) ) ;
#4180=ORIENTED_EDGE ( 'NONE', *, *, #9449, .F. ) ;
#4188=ORIENTED_EDGE ( 'NONE', *, *, #3717, .T. ) ;
#4194=DIRECTION ( 'NONE',  ( -1.000000000000000000, 0.000000000000000000, 0.000000000000000000 ) ) ;
#4195=EDGE_CURVE ( 'NONE', #4264, #1798, #70, .T. ) ;
#4196=EDGE_LOOP ( 'NONE', ( #8551, #786, #8226, #10022 ) ) ;
#4197=CARTESIAN_POINT ( 'NONE',  ( -10.00000000000000000, 0.000000000000000000, 0.000000000000000000 ) ) ;
#4201=DIRECTION ( 'NONE',  ( -1.000000000000000000, -0.000000000000000000, -0.000000000000000000 ) ) ;
#4202=DIRECTION ( 'NONE',  ( -1.000000000000000000, 0.000000000000000000, 0.000000000000000000 ) ) ;
#4204=ORIENTED_EDGE ( 'NONE', *, *, #2272, .F. ) ;
#4212=AXIS2_PLACEMENT_3D ( 'NONE', #7236, #4470, #3663 ) ;
#4220=AXIS2_PLACEMENT_3D ( 'NONE', #1203, #6961, #8911 ) ;
#4221=CARTESIAN_POINT ( 'NONE',  ( 4.999999999999997335, 6.123233995736766282E-16, -5.000000000000000000 ) ) ;
#4230=DIRECTION ( 'NONE',  ( 1.000000000000000000, 0.000000000000000000, 0.000000000000000000 ) ) ;
#4237=AXIS2_PLACEMENT_3D ( 'NONE', #8214, #6579, #11136 ) ;
#4243=VERTEX_POINT ( 'NONE', #4813 ) ;
#4245=FACE_OUTER_BOUND ( 'NONE', #12301, .T. ) ;
#4247=CARTESIAN_POINT ( 'NONE',  ( 4.999999999999999112, 2.791921004064568113, -22.37914155802282323 ) ) ;
#4260=DIRECTION ( 'NONE',  ( -1.000000000000000000, 0.000000000000000000, 0.000000000000000000 ) ) ;
#4264=VERTEX_POINT ( 'NONE', #2072 ) ;
#4265=CARTESIAN_POINT ( 'NONE',  ( 4.999999999999999112, 0.000000000000000000, 0.000000000000000000 ) ) ;
#4269=EDGE_CURVE ( 'NONE', #11016, #8473, #5819, .T. ) ;
#4271=LINE ( 'NONE', #9860, #8444 ) ;
#4282=AXIS2_PLACEMENT_3D ( 'NONE', #3457, #3382, #1456 ) ;
#4284=DIRECTION ( 'NONE',  ( -1.000000000000000000, 0.000000000000000000, 0.000000000000000000 ) ) ;
#4286=FACE_OUTER_BOUND ( 'NONE', #11466, .T. ) ;
#4289=ORIENTED_EDGE ( 'NONE', *, *, #10196, .F. ) ;
#4290=CARTESIAN_POINT ( 'NONE',  ( 4.999999999999999112, 0.000000000000000000, 20.24900000002024569 ) ) ;
#4291=AXIS2_PLACEMENT_3D ( 'NONE', #10989, #5439, #9263 ) ;
#4301=DIRECTION ( 'NONE',  ( 0.000000000000000000, -1.000000000000000000, -0.000000000000000000 ) ) ;
#4328=VERTEX_POINT ( 'NONE', #6999 ) ;
#4331=VERTEX_POINT ( 'NONE', #2124 ) ;
#4332=CARTESIAN_POINT ( 'NONE',  ( 4.999999999999999112, -22.83261415639512748, 14.41081992069301876 ) ) ;
#4338=CARTESIAN_POINT ( 'NONE',  ( 2.499999999999999556, 15.57980286237472711, 22.05152472667135655 ) ) ;
#4342=CARTESIAN_POINT ( 'NONE',  ( 0.000000000000000000, 20.18872947935930995, -1.561154383803291967 ) ) ;
#4346=DIRECTION ( 'NONE',  ( 0.000000000000000000, 0.000000000000000000, 1.000000000000000000 ) ) ;
#4352=CARTESIAN_POINT ( 'NONE',  ( 0.000000000000000000, -2.791921004064099154, -22.37914155802288363 ) ) ;
#4355=AXIS2_PLACEMENT_3D ( 'NONE', #3994, #8699, #121 ) ;
#4357=DIRECTION ( 'NONE',  ( 0.000000000000000000, 0.9238795325112851842, 0.3826834323650938896 ) ) ;
#4360=CARTESIAN_POINT ( 'NONE',  ( 4.999999999999999112, -2.791921004064099154, -22.37914155802288363 ) ) ;
#4367=VERTEX_POINT ( 'NONE', #11223 ) ;
#4369=ADVANCED_FACE ( 'NONE', ( #9245 ), #8351, .T. ) ;
#4373=VERTEX_POINT ( 'NONE', #5488 ) ;
#4375=AXIS2_PLACEMENT_3D ( 'NONE', #11115, #10246, #546 ) ;
#4377=ORIENTED_EDGE ( 'NONE', *, *, #7000, .F. ) ;
#4382=DIRECTION ( 'NONE',  ( -1.000000000000000000, -0.000000000000000000, 0.000000000000000000 ) ) ;
#4386=CARTESIAN_POINT ( 'NONE',  ( 4.999999999999999112, -26.60936692326686881, -4.576198416197525098 ) ) ;
#4400=CIRCLE ( 'NONE', #7205, 20.24900000002024569 ) ;
#4401=CARTESIAN_POINT ( 'NONE',  ( 4.999999999999999112, 0.000000000000000000, 0.000000000000000000 ) ) ;
#4402=DIRECTION ( 'NONE',  ( -1.000000000000000000, 0.000000000000000000, 0.000000000000000000 ) ) ;
#4405=DIRECTION ( 'NONE',  ( -1.000000000000000000, -0.000000000000000000, 0.000000000000000000 ) ) ;
#4407=AXIS2_PLACEMENT_3D ( 'NONE', #10353, #8498, #9196 ) ;
#4408=CARTESIAN_POINT ( 'NONE',  ( 4.999999999999999112, 0.000000000000000000, 0.000000000000000000 ) ) ;
#4424=ADVANCED_FACE ( 'NONE', ( #5421 ), #10338, .T. ) ;
#4428=AXIS2_PLACEMENT_3D ( 'NONE', #11625, #1945, #10560 ) ;
#4438=CARTESIAN_POINT ( 'NONE',  ( 4.999999999999999112, 5.955107813822865914, -26.33508479058314222 ) ) ;
#4444=VERTEX_POINT ( 'NONE', #10871 ) ;
#4449=AXIS2_PLACEMENT_3D ( 'NONE', #11918, #3324, #6080 ) ;
#4461=ORIENTED_EDGE ( 'NONE', *, *, #2329, .T. ) ;
#4463=CARTESIAN_POINT ( 'NONE',  ( 2.500000000000000444, -26.60936692326693631, 4.576198416197160057 ) ) ;
#4464=VERTEX_POINT ( 'NONE', #3854 ) ;
#4470=DIRECTION ( 'NONE',  ( -1.000000000000000000, -0.000000000000000000, -0.000000000000000000 ) ) ;
#4472=DIRECTION ( 'NONE',  ( 0.000000000000000000, -0.3826834323650774028, -0.9238795325112918455 ) ) ;
#4474=EDGE_CURVE ( 'NONE', #5247, #8156, #5074, .T. ) ;
#4484=VECTOR ( 'NONE', #5842, 1000.000000000000000 ) ;
#4487=EDGE_CURVE ( 'NONE', #2987, #3057, #11658, .T. ) ;
#4488=EDGE_CURVE ( 'NONE', #10481, #2061, #9733, .T. ) ;
#4492=VERTEX_POINT ( 'NONE', #3783 ) ;
#4497=DIRECTION ( 'NONE',  ( 0.000000000000000000, 0.000000000000000000, 1.000000000000000000 ) ) ;
#4505=ORIENTED_EDGE ( 'NONE', *, *, #4582, .F. ) ;
#4510=CYLINDRICAL_SURFACE ( 'NONE', #4282, 9.600000000009600853 ) ;
#4513=CARTESIAN_POINT ( 'NONE',  ( 4.999999999999999112, -9.168210874537443544, -18.05452603534175537 ) ) ;
#4517=FACE_OUTER_BOUND ( 'NONE', #8619, .T. ) ;
#4521=EDGE_LOOP ( 'NONE', ( #8180, #11265, #910, #2539 ) ) ;
#4522=CARTESIAN_POINT ( 'NONE',  ( 4.999999999999999112, 0.000000000000000000, 0.000000000000000000 ) ) ;
#4529=CARTESIAN_POINT ( 'NONE',  ( 4.999999999999999112, 5.984728032765264771, -21.74405275335751853 ) ) ;
#4532=DIRECTION ( 'NONE',  ( 0.000000000000000000, 0.3826834323650905589, -0.9238795325112864054 ) ) ;
#4537=ORIENTED_EDGE ( 'NONE', *, *, #8612, .F. ) ;
#4539=EDGE_CURVE ( 'NONE', #7704, #7924, #1282, .T. ) ;
#4553=CARTESIAN_POINT ( 'NONE',  ( 4.999999999999999112, 26.33508479058320617, 5.955107813822601237 ) ) ;
#4557=AXIS2_PLACEMENT_3D ( 'NONE', #208, #3286, #7857 ) ;
#4558=DIRECTION ( 'NONE',  ( -1.000000000000000000, -0.000000000000000000, -0.000000000000000000 ) ) ;
#4559=DIRECTION ( 'NONE',  ( -1.000000000000000000, 0.000000000000000000, 0.000000000000000000 ) ) ;
#4565=DIRECTION ( 'NONE',  ( -1.000000000000000000, 0.000000000000000000, -0.000000000000000000 ) ) ;
#4571=LINE ( 'NONE', #8331, #10381 ) ;
#4575=DIRECTION ( 'NONE',  ( 0.000000000000000000, 0.000000000000000000, 1.000000000000000000 ) ) ;
#4582=EDGE_CURVE ( 'NONE', #1798, #238, #10465, .T. ) ;
#4593=ORIENTED_EDGE ( 'NONE', *, *, #9578, .F. ) ;
#4594=VERTEX_POINT ( 'NONE', #1334 ) ;
#4595=CYLINDRICAL_SURFACE ( 'NONE', #7223, 27.00000000002699707 ) ;
#4601=CIRCLE ( 'NONE', #3403, 20.24900000002024569 ) ;
#4603=CARTESIAN_POINT ( 'NONE',  ( 2.499999999999999556, 26.60936692326690789, -4.576198416197345686 ) ) ;
#4604=AXIS2_PLACEMENT_3D ( 'NONE', #7782, #4026, #4955 ) ;
#4609=CIRCLE ( 'NONE', #5811, 9.600000000009600853 ) ;
#4621=VERTEX_POINT ( 'NONE', #9864 ) ;
#4644=CIRCLE ( 'NONE', #9640, 5.000000000000000000 ) ;
#4668=DIRECTION ( 'NONE',  ( 0.000000000000000000, 0.000000000000000000, 1.000000000000000000 ) ) ;
#4670=DIRECTION ( 'NONE',  ( 0.000000000000000000, 0.000000000000000000, 1.000000000000000000 ) ) ;
#4681=FACE_OUTER_BOUND ( 'NONE', #12214, .T. ) ;
#4685=ORIENTED_EDGE ( 'NONE', *, *, #9868, .F. ) ;
#4688=AXIS2_PLACEMENT_3D ( 'NONE', #12065, #628, #745 ) ;
#4695=CARTESIAN_POINT ( 'NONE',  ( 4.999999999999999112, 14.41081992069340600, -22.83261415639488234 ) ) ;
#4697=ORIENTED_EDGE ( 'NONE', *, *, #11492, .T. ) ;
#4702=FACE_OUTER_BOUND ( 'NONE', #8390, .T. ) ;
#4719=VERTEX_POINT ( 'NONE', #4332 ) ;
#4720=VERTEX_POINT ( 'NONE', #760 ) ;
#4722=VERTEX_POINT ( 'NONE', #10211 ) ;
#4726=ADVANCED_FACE ( 'NONE', ( #12131 ), #8223, .T. ) ;
#4729=FACE_OUTER_BOUND ( 'NONE', #10137, .T. ) ;
#4749=LINE ( 'NONE', #8571, #6459 ) ;
#4757=ADVANCED_FACE ( 'NONE', ( #1710 ), #6343, .T. ) ;
#4758=CARTESIAN_POINT ( 'NONE',  ( 0.000000000000000000, -13.17168466712917585, -15.37949036966225513 ) ) ;
#4759=LINE ( 'NONE', #81, #10038 ) ;
#4765=ORIENTED_EDGE ( 'NONE', *, *, #2720, .T. ) ;
#4767=CIRCLE ( 'NONE', #6363, 9.600000000009600853 ) ;
#4773=EDGE_CURVE ( 'NONE', #7692, #6998, #9291, .T. ) ;
#4774=VECTOR ( 'NONE', #581, 1000.000000000000000 ) ;
#4782=VERTEX_POINT ( 'NONE', #3839 ) ;
#4785=ORIENTED_EDGE ( 'NONE', *, *, #666, .T. ) ;
#4794=DIRECTION ( 'NONE',  ( 0.000000000000000000, 0.000000000000000000, 1.000000000000000000 ) ) ;
#4797=ORIENTED_EDGE ( 'NONE', *, *, #3568, .F. ) ;
#4799=CARTESIAN_POINT ( 'NONE',  ( 4.999999999999997335, 4.769696007084728073, -1.500000000000000000 ) ) ;
#4802=DIRECTION ( 'NONE',  ( -1.000000000000000000, 0.000000000000000000, 0.000000000000000000 ) ) ;
#4807=DIRECTION ( 'NONE',  ( 0.000000000000000000, -0.7071067811865389130, -0.7071067811865562325 ) ) ;
#4813=CARTESIAN_POINT ( 'NONE',  ( 4.999999999999999112, 5.955107813822506202, 26.33508479058322393 ) ) ;
#4817=CIRCLE ( 'NONE', #2814, 9.600000000009600853 ) ;
#4822=CIRCLE ( 'NONE', #222, 27.00000000002699707 ) ;
#4834=AXIS2_PLACEMENT_3D ( 'NONE', #3033, #22, #1913 ) ;
#4837=CIRCLE ( 'NONE', #424, 20.24900000002024569 ) ;
#4838=AXIS2_PLACEMENT_3D ( 'NONE', #1760, #7219, #2459 ) ;
#4840=EDGE_CURVE ( 'NONE', #2049, #8321, #8893, .T. ) ;
#4847=LINE ( 'NONE', #2961, #3837 ) ;
#4852=DIRECTION ( 'NONE',  ( 1.000000000000000000, -0.000000000000000000, 0.000000000000000000 ) ) ;
#4862=CARTESIAN_POINT ( 'NONE',  ( 4.999999999999999112, -20.18872947935932061, 1.561154383803151191 ) ) ;
#4864=DIRECTION ( 'NONE',  ( -1.000000000000000000, -0.000000000000000000, -0.000000000000000000 ) ) ;
#4865=FACE_OUTER_BOUND ( 'NONE', #2528, .T. ) ;
#4868=FACE_OUTER_BOUND ( 'NONE', #2466, .T. ) ;
#4869=ORIENTED_EDGE ( 'NONE', *, *, #2634, .T. ) ;
#4875=EDGE_CURVE ( 'NONE', #4594, #12228, #7093, .T. ) ;
#4876=EDGE_CURVE ( 'NONE', #4373, #6551, #1016, .T. ) ;
#4878=ORIENTED_EDGE ( 'NONE', *, *, #11375, .T. ) ;
#4879=DIRECTION ( 'NONE',  ( 1.000000000000000000, 0.000000000000000000, 0.000000000000000000 ) ) ;
#4881=EDGE_LOOP ( 'NONE', ( #4990, #895, #10528, #12116 ) ) ;
#4882=AXIS2_PLACEMENT_3D ( 'NONE', #8659, #3904, #2955 ) ;
#4883=DIRECTION ( 'NONE',  ( 0.000000000000000000, 0.000000000000000000, 1.000000000000000000 ) ) ;
#4892=CARTESIAN_POINT ( 'NONE',  ( 4.999999999999999112, 19.24938187143305512, -6.283573709965099674 ) ) ;
#4898=DIRECTION ( 'NONE',  ( 0.000000000000000000, -0.9238795325112826307, -0.3826834323650997183 ) ) ;
#4904=LINE ( 'NONE', #7595, #2359 ) ;
#4906=PLANE ( 'NONE',  #7238 ) ;
#4915=ORIENTED_EDGE ( 'NONE', *, *, #3102, .T. ) ;
#4920=ADVANCED_FACE ( 'NONE', ( #6775 ), #6850, .F. ) ;
#4928=CARTESIAN_POINT ( 'NONE',  ( 0.000000000000000000, 19.24938187143305512, -6.283573709965099674 ) ) ;
#4930=EDGE_CURVE ( 'NONE', #1981, #536, #6697, .T. ) ;
#4932=CARTESIAN_POINT ( 'NONE',  ( 0.000000000000000000, 19.60720892790252989, 11.14352537685181588 ) ) ;
#4935=CARTESIAN_POINT ( 'NONE',  ( 50.00005079999999680, 6.799999999999999822, -1.500000000000000000 ) ) ;
#4940=DIRECTION ( 'NONE',  ( -1.000000000000000000, 0.000000000000000000, 0.000000000000000000 ) ) ;
#4947=CARTESIAN_POINT ( 'NONE',  ( 2.499999999999999556, 22.83261415639523051, -14.41081992069285178 ) ) ;
#4948=ORIENTED_EDGE ( 'NONE', *, *, #8595, .T. ) ;
#4955=DIRECTION ( 'NONE',  ( 0.000000000000000000, 0.000000000000000000, 1.000000000000000000 ) ) ;
#4956=LINE ( 'NONE', #9908, #8564 ) ;
#4961=CIRCLE ( 'NONE', #5363, 9.600000000009604406 ) ;
#4970=CIRCLE ( 'NONE', #1775, 27.00000000002699707 ) ;
#4971=DIRECTION ( 'NONE',  ( 0.000000000000000000, 0.000000000000000000, 1.000000000000000000 ) ) ;
#4972=ORIENTED_EDGE ( 'NONE', *, *, #1755, .T. ) ;
#4975=CARTESIAN_POINT ( 'NONE',  ( 50.00005079999999680, 0.000000000000000000, 0.000000000000000000 ) ) ;
#4977=ORIENTED_EDGE ( 'NONE', *, *, #3902, .F. ) ;
#4982=AXIS2_PLACEMENT_3D ( 'NONE', #9869, #5528, #11036 ) ;
#4990=ORIENTED_EDGE ( 'NONE', *, *, #10346, .F. ) ;
#4991=CARTESIAN_POINT ( 'NONE',  ( 0.000000000000000000, 0.000000000000000000, 0.000000000000000000 ) ) ;
#5009=DIRECTION ( 'NONE',  ( -1.000000000000000000, 0.000000000000000000, -0.000000000000000000 ) ) ;
#5016=VERTEX_POINT ( 'NONE', #2087 ) ;
#5018=AXIS2_PLACEMENT_3D ( 'NONE', #5797, #8683, #10785 ) ;
#5019=AXIS2_PLACEMENT_3D ( 'NONE', #8740, #3981, #12315 ) ;
#5022=EDGE_CURVE ( 'NONE', #11273, #2049, #11465, .T. ) ;
#5026=CARTESIAN_POINT ( 'NONE',  ( 4.999999999999999112, 21.74405275335758247, 5.984728032765037398 ) ) ;
#5045=DIRECTION ( 'NONE',  ( 0.000000000000000000, 0.000000000000000000, 1.000000000000000000 ) ) ;
#5047=DIRECTION ( 'NONE',  ( -1.000000000000000000, -0.000000000000000000, -0.000000000000000000 ) ) ;
#5059=CYLINDRICAL_SURFACE ( 'NONE', #4, 5.000000000000000000 ) ;
#5060=CIRCLE ( 'NONE', #8871, 20.24900000002024569 ) ;
#5064=ORIENTED_EDGE ( 'NONE', *, *, #8383, .T. ) ;
#5070=CARTESIAN_POINT ( 'NONE',  ( 4.999999999999999112, -18.05452603534159195, -9.168210874537770394 ) ) ;
#5072=DIRECTION ( 'NONE',  ( -1.000000000000000000, 0.000000000000000000, -0.000000000000000000 ) ) ;
#5074=CIRCLE ( 'NONE', #5885, 9.600000000009600853 ) ;
#5077=ORIENTED_EDGE ( 'NONE', *, *, #9470, .T. ) ;
#5087=CARTESIAN_POINT ( 'NONE',  ( -10.00000000000000000, 0.000000000000000000, 0.000000000000000000 ) ) ;
#5090=DIRECTION ( 'NONE',  ( -1.000000000000000000, 0.000000000000000000, -0.000000000000000000 ) ) ;
#5092=AXIS2_PLACEMENT_3D ( 'NONE', #10086, #4565, #2449 ) ;
#5095=ADVANCED_FACE ( 'NONE', ( #5328 ), #2376, .T. ) ;
#5102=DIRECTION ( 'NONE',  ( 0.000000000000000000, 0.000000000000000000, 1.000000000000000000 ) ) ;
#5106=ORIENTED_EDGE ( 'NONE', *, *, #5554, .T. ) ;
#5107=ADVANCED_FACE ( 'NONE', ( #11927 ), #4510, .T. ) ;
#5112=CARTESIAN_POINT ( 'NONE',  ( 0.000000000000000000, 9.168210874537823685, -18.05452603534156353 ) ) ;
#5113=DIRECTION ( 'NONE',  ( 1.000000000000000000, 0.000000000000000000, -0.000000000000000000 ) ) ;
#5117=CARTESIAN_POINT ( 'NONE',  ( 0.000000000000000000, 21.74405275335766419, -5.984728032764733641 ) ) ;
#5126=CARTESIAN_POINT ( 'NONE',  ( 2.499999999999999556, 15.57980286237503620, -22.05152472667113983 ) ) ;
#5130=ORIENTED_EDGE ( 'NONE', *, *, #2329, .F. ) ;
#5140=CYLINDRICAL_SURFACE ( 'NONE', #6003, 9.600000000009600853 ) ;
#5144=DIRECTION ( 'NONE',  ( 0.000000000000000000, 0.7071067811865486830, -0.7071067811865463515 ) ) ;
#5150=ADVANCED_FACE ( 'NONE', ( #1565 ), #9208, .T. ) ;
#5158=LINE ( 'NONE', #7053, #12184 ) ;
#5161=DIRECTION ( 'NONE',  ( -1.000000000000000000, -0.000000000000000000, 0.000000000000000000 ) ) ;
#5165=AXIS2_PLACEMENT_3D ( 'NONE', #350, #239, #9933 ) ;
#5166=CARTESIAN_POINT ( 'NONE',  ( 0.000000000000000000, -17.79862902732275032, 13.85025647830051021 ) ) ;
#5169=CARTESIAN_POINT ( 'NONE',  ( 4.999999999999999112, -20.18872947935932061, 1.561154383803151191 ) ) ;
#5182=EDGE_CURVE ( 'NONE', #7570, #12046, #7101, .T. ) ;
#5188=CARTESIAN_POINT ( 'NONE',  ( 0.000000000000000000, 5.984728032764962791, 21.74405275335760379 ) ) ;
#5191=ORIENTED_EDGE ( 'NONE', *, *, #1326, .T. ) ;
#5193=CARTESIAN_POINT ( 'NONE',  ( 4.999999999999999112, 15.57980286237503620, -22.05152472667113628 ) ) ;
#5202=DIRECTION ( 'NONE',  ( -1.000000000000000000, 0.000000000000000000, 0.000000000000000000 ) ) ;
#5209=CIRCLE ( 'NONE', #813, 9.600000000009602630 ) ;
#5215=CIRCLE ( 'NONE', #11596, 9.600000000009600853 ) ;
#5222=CARTESIAN_POINT ( 'NONE',  ( 2.499999999999999556, -15.57980286237488343, 22.05152472667124997 ) ) ;
#5227=DIRECTION ( 'NONE',  ( -1.000000000000000000, 0.000000000000000000, 0.000000000000000000 ) ) ;
#5233=ORIENTED_EDGE ( 'NONE', *, *, #8647, .F. ) ;
#5236=CARTESIAN_POINT ( 'NONE',  ( 2.500000000000000444, 4.576198416197625463, -26.60936692326685815 ) ) ;
#5246=AXIS2_PLACEMENT_3D ( 'NONE', #4408, #5161, #1408 ) ;
#5247=VERTEX_POINT ( 'NONE', #10504 ) ;
#5251=CARTESIAN_POINT ( 'NONE',  ( 4.999999999999999112, 15.57980286237472889, 22.05152472667134944 ) ) ;
#5256=PLANE ( 'NONE',  #10547 ) ;
#5258=EDGE_CURVE ( 'NONE', #6501, #11122, #1889, .T. ) ;
#5259=CIRCLE ( 'NONE', #6868, 20.24900000002024569 ) ;
#5263=CARTESIAN_POINT ( 'NONE',  ( 2.500000000000000444, -14.41081992069293349, -22.83261415639518432 ) ) ;
#5265=EDGE_LOOP ( 'NONE', ( #11591, #8959, #69, #5106 ) ) ;
#5272=ORIENTED_EDGE ( 'NONE', *, *, #8852, .T. ) ;
#5275=CYLINDRICAL_SURFACE ( 'NONE', #7239, 27.00000000002699707 ) ;
#5280=CARTESIAN_POINT ( 'NONE',  ( 4.999999999999999112, 5.984728032764962791, 21.74405275335760379 ) ) ;
#5281=ORIENTED_EDGE ( 'NONE', *, *, #2517, .F. ) ;
#5285=ORIENTED_EDGE ( 'NONE', *, *, #11177, .T. ) ;
#5289=EDGE_LOOP ( 'NONE', ( #6984, #10533, #5337, #5565 ) ) ;
#5291=CARTESIAN_POINT ( 'NONE',  ( 0.000000000000000000, -15.57980286237457257, -22.05152472667146668 ) ) ;
#5294=LINE ( 'NONE', #7052, #5613 ) ;
#5298=ORIENTED_EDGE ( 'NONE', *, *, #5785, .F. ) ;
#5310=VERTEX_POINT ( 'NONE', #4695 ) ;
#5311=FACE_OUTER_BOUND ( 'NONE', #1599, .T. ) ;
#5318=EDGE_CURVE ( 'NONE', #908, #1305, #898, .T. ) ;
#5319=ADVANCED_FACE ( 'NONE', ( #11255 ), #8515, .T. ) ;
#5328=FACE_OUTER_BOUND ( 'NONE', #11154, .T. ) ;
#5332=LINE ( 'NONE', #568, #11573 ) ;
#5335=DIRECTION ( 'NONE',  ( -1.000000000000000000, 0.000000000000000000, 0.000000000000000000 ) ) ;
#5337=ORIENTED_EDGE ( 'NONE', *, *, #148, .T. ) ;
#5338=DIRECTION ( 'NONE',  ( 0.000000000000000000, 0.000000000000000000, 1.000000000000000000 ) ) ;
#5347=DIRECTION ( 'NONE',  ( 1.000000000000000000, 0.000000000000000000, 0.000000000000000000 ) ) ;
#5348=CARTESIAN_POINT ( 'NONE',  ( 0.000000000000000000, -2.791921004064401579, 22.37914155802284100 ) ) ;
#5349=DIRECTION ( 'NONE',  ( -1.000000000000000000, 0.000000000000000000, 0.000000000000000000 ) ) ;
#5356=LINE ( 'NONE', #4290, #9231 ) ;
#5361=ORIENTED_EDGE ( 'NONE', *, *, #9449, .T. ) ;
#5363=AXIS2_PLACEMENT_3D ( 'NONE', #10865, #1168, #3989 ) ;
#5365=AXIS2_PLACEMENT_3D ( 'NONE', #1303, #354, #4173 ) ;
#5367=CIRCLE ( 'NONE', #10348, 20.24900000002024569 ) ;
#5374=AXIS2_PLACEMENT_3D ( 'NONE', #4991, #9818, #10869 ) ;
#5377=CARTESIAN_POINT ( 'NONE',  ( 0.000000000000000000, 0.000000000000000000, 0.000000000000000000 ) ) ;
#5382=DIRECTION ( 'NONE',  ( -1.000000000000000000, 0.000000000000000000, 0.000000000000000000 ) ) ;
#5383=ORIENTED_EDGE ( 'NONE', *, *, #3999, .T. ) ;
#5385=AXIS2_PLACEMENT_3D ( 'NONE', #6007, #6898, #8897 ) ;
#5386=EDGE_CURVE ( 'NONE', #9862, #997, #2685, .T. ) ;
#5397=DIRECTION ( 'NONE',  ( 0.000000000000000000, 0.000000000000000000, -1.000000000000000000 ) ) ;
#5400=CARTESIAN_POINT ( 'NONE',  ( 0.000000000000000000, 22.05152472667129970, 15.57980286237480350 ) ) ;
#5408=EDGE_CURVE ( 'NONE', #5656, #7570, #3261, .T. ) ;
#5413=CARTESIAN_POINT ( 'NONE',  ( 0.000000000000000000, -26.33508479058316709, -5.955107813822780649 ) ) ;
#5421=FACE_OUTER_BOUND ( 'NONE', #3387, .T. ) ;
#5425=DIRECTION ( 'NONE',  ( 0.000000000000000000, 0.000000000000000000, 1.000000000000000000 ) ) ;
#5430=CARTESIAN_POINT ( 'NONE',  ( 4.999999999999999112, -15.57980286237457257, -22.05152472667146313 ) ) ;
#5431=ORIENTED_EDGE ( 'NONE', *, *, #11654, .T. ) ;
#5437=CIRCLE ( 'NONE', #39, 9.600000000009600853 ) ;
#5439=DIRECTION ( 'NONE',  ( -1.000000000000000000, 0.000000000000000000, 0.000000000000000000 ) ) ;
#5457=AXIS2_PLACEMENT_3D ( 'NONE', #11367, #11439, #10501 ) ;
#5458=ORIENTED_EDGE ( 'NONE', *, *, #11513, .F. ) ;
#5465=CYLINDRICAL_SURFACE ( 'NONE', #11423, 20.24900000002024569 ) ;
#5471=ORIENTED_EDGE ( 'NONE', *, *, #78, .T. ) ;
#5473=ORIENTED_EDGE ( 'NONE', *, *, #6020, .F. ) ;
#5477=FACE_OUTER_BOUND ( 'NONE', #2003, .T. ) ;
#5479=CARTESIAN_POINT ( 'NONE',  ( 2.499999999999999556, 26.60936692326690789, 4.576198416197345686 ) ) ;
#5483=AXIS2_PLACEMENT_3D ( 'NONE', #10531, #3915, #9488 ) ;
#5486=ADVANCED_FACE ( 'NONE', ( #10875 ), #2304, .T. ) ;
#5488=CARTESIAN_POINT ( 'NONE',  ( 0.000000000000000000, -22.05152472667140984, 15.57980286237465073 ) ) ;
#5495=DIRECTION ( 'NONE',  ( -1.000000000000000000, 0.000000000000000000, 0.000000000000000000 ) ) ;
#5497=ORIENTED_EDGE ( 'NONE', *, *, #6498, .F. ) ;
#5499=ORIENTED_EDGE ( 'NONE', *, *, #5386, .F. ) ;
#5502=EDGE_LOOP ( 'NONE', ( #1737, #926, #3046, #1922 ) ) ;
#5505=ADVANCED_FACE ( 'NONE', ( #1361 ), #9008, .T. ) ;
#5507=CYLINDRICAL_SURFACE ( 'NONE', #564, 20.24900000002024569 ) ;
#5510=ORIENTED_EDGE ( 'NONE', *, *, #5182, .F. ) ;
#5514=VERTEX_POINT ( 'NONE', #3501 ) ;
#5516=CARTESIAN_POINT ( 'NONE',  ( 0.000000000000000000, -20.18872947935930284, -1.561154383803435408 ) ) ;
#5528=DIRECTION ( 'NONE',  ( -1.000000000000000000, 0.000000000000000000, -0.000000000000000000 ) ) ;
#5535=DIRECTION ( 'NONE',  ( 0.000000000000000000, 1.000000000000000000, 0.000000000000000000 ) ) ;
#5543=EDGE_CURVE ( 'NONE', #6125, #3907, #9701, .T. ) ;
#5552=ORIENTED_EDGE ( 'NONE', *, *, #2433, .T. ) ;
#5553=CARTESIAN_POINT ( 'NONE',  ( 4.999999999999999112, -19.24938187143291657, -6.283573709965514453 ) ) ;
#5554=EDGE_CURVE ( 'NONE', #8041, #9710, #6305, .T. ) ;
#5561=DIRECTION ( 'NONE',  ( -1.000000000000000000, 0.000000000000000000, 0.000000000000000000 ) ) ;
#5562=CARTESIAN_POINT ( 'NONE',  ( 2.499999999999999556, -26.33508479058324880, 5.955107813822412943 ) ) ;
#5564=ADVANCED_FACE ( 'NONE', ( #11979 ), #10176, .T. ) ;
#5565=ORIENTED_EDGE ( 'NONE', *, *, #6088, .T. ) ;
#5569=AXIS2_PLACEMENT_3D ( 'NONE', #4932, #4879, #67 ) ;
#5575=CIRCLE ( 'NONE', #10364, 9.600000000009600853 ) ;
#5588=DIRECTION ( 'NONE',  ( -1.000000000000000000, 0.000000000000000000, 0.000000000000000000 ) ) ;
#5593=DIRECTION ( 'NONE',  ( -1.000000000000000000, -0.000000000000000000, -0.000000000000000000 ) ) ;
#5596=DIRECTION ( 'NONE',  ( 0.000000000000000000, 0.000000000000000000, 1.000000000000000000 ) ) ;
#5608=ADVANCED_FACE ( 'NONE', ( #5311 ), #9130, .T. ) ;
#5613=VECTOR ( 'NONE', #585, 1000.000000000000000 ) ;
#5614=CARTESIAN_POINT ( 'NONE',  ( 4.999999999999999112, 18.05452603534165945, 9.168210874537644273 ) ) ;
#5624=CIRCLE ( 'NONE', #1841, 27.00000000002699707 ) ;
#5631=FACE_OUTER_BOUND ( 'NONE', #4881, .T. ) ;
#5635=ORIENTED_EDGE ( 'NONE', *, *, #1743, .F. ) ;
#5640=CIRCLE ( 'NONE', #4838, 27.00000000002699707 ) ;
#5645=DIRECTION ( 'NONE',  ( -1.000000000000000000, -0.000000000000000000, 0.000000000000000000 ) ) ;
#5652=DIRECTION ( 'NONE',  ( 0.000000000000000000, -1.000000000000000000, 0.000000000000000000 ) ) ;
#5656=VERTEX_POINT ( 'NONE', #11429 ) ;
#5660=CARTESIAN_POINT ( 'NONE',  ( 0.000000000000000000, -6.283573709965444287, 19.24938187143293788 ) ) ;
#5662=DIRECTION ( 'NONE',  ( 0.000000000000000000, 0.3826834323650841196, 0.9238795325112890700 ) ) ;
#5666=CARTESIAN_POINT ( 'NONE',  ( 4.999999999999999112, 1.561154383803221579, 20.18872947935931705 ) ) ;
#5671=VERTEX_POINT ( 'NONE', #11242 ) ;
#5672=CYLINDRICAL_SURFACE ( 'NONE', #9367, 9.600000000009600853 ) ;
#5680=CARTESIAN_POINT ( 'NONE',  ( 4.999999999999999112, -11.14352537685188338, 19.60720892790249081 ) ) ;
#5684=AXIS2_PLACEMENT_3D ( 'NONE', #4522, #8340, #3399 ) ;
#5693=ORIENTED_EDGE ( 'NONE', *, *, #687, .T. ) ;
#5694=ORIENTED_EDGE ( 'NONE', *, *, #2118, .F. ) ;
#5702=EDGE_CURVE ( 'NONE', #2216, #10868, #3743, .T. ) ;
#5703=FACE_OUTER_BOUND ( 'NONE', #1948, .T. ) ;
#5707=ORIENTED_EDGE ( 'NONE', *, *, #10894, .F. ) ;
#5715=DIRECTION ( 'NONE',  ( -1.000000000000000000, -0.000000000000000000, 0.000000000000000000 ) ) ;
#5720=VERTEX_POINT ( 'NONE', #8561 ) ;
#5725=EDGE_LOOP ( 'NONE', ( #288, #3925, #479, #12264, #10848, #1200 ) ) ;
#5727=CARTESIAN_POINT ( 'NONE',  ( 4.999999999999999112, 5.984728032765264771, -21.74405275335751853 ) ) ;
#5750=EDGE_CURVE ( 'NONE', #9337, #138, #12233, .T. ) ;
#5758=CARTESIAN_POINT ( 'NONE',  ( 2.499999999999999556, 5.955107813822504426, 26.33508479058322749 ) ) ;
#5759=ORIENTED_EDGE ( 'NONE', *, *, #10968, .T. ) ;
#5761=CARTESIAN_POINT ( 'NONE',  ( 0.000000000000000000, 5.984728032765264771, -21.74405275335751853 ) ) ;
#5769=ORIENTED_EDGE ( 'NONE', *, *, #11051, .F. ) ;
#5774=CYLINDRICAL_SURFACE ( 'NONE', #4604, 9.600000000009600853 ) ;
#5778=DIRECTION ( 'NONE',  ( 0.000000000000000000, 0.000000000000000000, 1.000000000000000000 ) ) ;
#5781=EDGE_LOOP ( 'NONE', ( #8892, #1508, #1487, #7386 ) ) ;
#5785=EDGE_CURVE ( 'NONE', #4782, #4594, #12271, .T. ) ;
#5797=CARTESIAN_POINT ( 'NONE',  ( 0.000000000000000000, 0.000000000000000000, 0.000000000000000000 ) ) ;
#5804=DIRECTION ( 'NONE',  ( 0.000000000000000000, -6.982962677686267499E-15, 1.000000000000000000 ) ) ;
#5806=ORIENTED_EDGE ( 'NONE', *, *, #7106, .T. ) ;
#5807=LINE ( 'NONE', #9808, #10214 ) ;
#5810=AXIS2_PLACEMENT_3D ( 'NONE', #11812, #3269, #11989 ) ;
#5811=AXIS2_PLACEMENT_3D ( 'NONE', #2729, #3427, #10169 ) ;
#5819=LINE ( 'NONE', #4935, #1073 ) ;
#5820=AXIS2_PLACEMENT_3D ( 'NONE', #1718, #11153, #3535 ) ;
#5822=VECTOR ( 'NONE', #2711, 1000.000000000000000 ) ;
#5827=CIRCLE ( 'NONE', #3230, 27.00000000002699707 ) ;
#5829=PRODUCT_DEFINITION_SHAPE ( 'NONE', 'NONE',  #9774 ) ;
#5840=AXIS2_PLACEMENT_3D ( 'NONE', #5348, #2403, #9170 ) ;
#5841=ORIENTED_EDGE ( 'NONE', *, *, #2720, .F. ) ;
#5842=DIRECTION ( 'NONE',  ( 1.000000000000000000, -0.000000000000000000, -0.000000000000000000 ) ) ;
#5846=EDGE_CURVE ( 'NONE', #4782, #9862, #5807, .T. ) ;
#5848=CIRCLE ( 'NONE', #7447, 9.600000000009604406 ) ;
#5860=DIRECTION ( 'NONE',  ( 1.000000000000000000, 0.000000000000000000, 0.000000000000000000 ) ) ;
#5866=ORIENTED_EDGE ( 'NONE', *, *, #11735, .T. ) ;
#5878=DIRECTION ( 'NONE',  ( 0.000000000000000000, 1.000000000000000000, 3.614007241614733816E-15 ) ) ;
#5885=AXIS2_PLACEMENT_3D ( 'NONE', #2098, #5860, #9541 ) ;
#5892=AXIS2_PLACEMENT_3D ( 'NONE', #3281, #4194, #6908 ) ;
#5894=DIRECTION ( 'NONE',  ( 0.000000000000000000, 1.000000000000000000, 3.491481338843133750E-15 ) ) ;
#5899=AXIS2_PLACEMENT_3D ( 'NONE', #12304, #3823, #2692 ) ;
#5903=CARTESIAN_POINT ( 'NONE',  ( 0.000000000000000000, -22.37914155802283034, -2.791921004064479739 ) ) ;
#5914=CARTESIAN_POINT ( 'NONE',  ( 4.999999999999999112, 9.168210874537576771, 18.05452603534168432 ) ) ;
#5922=DIRECTION ( 'NONE',  ( -1.000000000000000000, -0.000000000000000000, -0.000000000000000000 ) ) ;
#5925=CARTESIAN_POINT ( 'NONE',  ( 4.999999999999999112, 13.17168466712950092, -15.37949036966198157 ) ) ;
#5934=EDGE_CURVE ( 'NONE', #8451, #486, #10113, .T. ) ;
#5939=ORIENTED_EDGE ( 'NONE', *, *, #5258, .F. ) ;
#5941=DIRECTION ( 'NONE',  ( -1.000000000000000000, -0.000000000000000000, 0.000000000000000000 ) ) ;
#5951=DIRECTION ( 'NONE',  ( -1.000000000000000000, 0.000000000000000000, 0.000000000000000000 ) ) ;
#5961=ORIENTED_EDGE ( 'NONE', *, *, #3515, .T. ) ;
#5964=CARTESIAN_POINT ( 'NONE',  ( 4.999999999999999112, 18.05452603534179090, -9.168210874537381372 ) ) ;
#5968=ORIENTED_EDGE ( 'NONE', *, *, #7710, .T. ) ;
#5970=VECTOR ( 'NONE', #5588, 1000.000000000000000 ) ;
#5975=CIRCLE ( 'NONE', #8777, 9.600000000009600853 ) ;
#5986=ORIENTED_EDGE ( 'NONE', *, *, #6261, .T. ) ;
#5993=EDGE_CURVE ( 'NONE', #4722, #7798, #7119, .T. ) ;
#5995=EDGE_CURVE ( 'NONE', #8081, #7435, #2419, .T. ) ;
#5998=DIRECTION ( 'NONE',  ( 1.000000000000000000, 0.000000000000000000, 0.000000000000000000 ) ) ;
#6003=AXIS2_PLACEMENT_3D ( 'NONE', #8965, #5202, #7032 ) ;
#6005=AXIS2_PLACEMENT_3D ( 'NONE', #3506, #11065, #2499 ) ;
#6007=CARTESIAN_POINT ( 'NONE',  ( 4.999999999999999112, 19.60720892790252989, -11.14352537685181588 ) ) ;
#6008=AXIS2_PLACEMENT_3D ( 'NONE', #8888, #3311, #3360 ) ;
#6018=DIRECTION ( 'NONE',  ( -1.000000000000000000, -0.000000000000000000, -0.000000000000000000 ) ) ;
#6019=DIRECTION ( 'NONE',  ( 0.000000000000000000, 0.000000000000000000, -1.000000000000000000 ) ) ;
#6020=EDGE_CURVE ( 'NONE', #10868, #1819, #9825, .T. ) ;
#6021=EDGE_LOOP ( 'NONE', ( #594, #7973, #3350, #9599 ) ) ;
#6033=EDGE_CURVE ( 'NONE', #8470, #2779, #11403, .T. ) ;
#6036=CARTESIAN_POINT ( 'NONE',  ( 4.999999999999999112, 17.79862902732265084, 13.85025647830063100 ) ) ;
#6038=CIRCLE ( 'NONE', #6638, 9.600000000009599077 ) ;
#6039=ORIENTED_EDGE ( 'NONE', *, *, #666, .F. ) ;
#6040=EDGE_LOOP ( 'NONE', ( #9176, #11357, #4869, #2789 ) ) ;
#6045=ADVANCED_FACE ( 'NONE', ( #10165 ), #11966, .T. ) ;
#6047=DIRECTION ( 'NONE',  ( -1.000000000000000000, -0.000000000000000000, 0.000000000000000000 ) ) ;
#6048=DIRECTION ( 'NONE',  ( 0.000000000000000000, -0.7071067811865536790, 0.7071067811865413555 ) ) ;
#6049=CARTESIAN_POINT ( 'NONE',  ( 50.00005079999999680, 0.000000000000000000, 1.500000000000000000 ) ) ;
#6052=ORIENTED_EDGE ( 'NONE', *, *, #10118, .T. ) ;
#6054=CIRCLE ( 'NONE', #653, 9.600000000009600853 ) ;
#6056=AXIS2_PLACEMENT_3D ( 'NONE', #212, #4035, #8864 ) ;
#6061=DIRECTION ( 'NONE',  ( -1.000000000000000000, 0.000000000000000000, 0.000000000000000000 ) ) ;
#6065=DIRECTION ( 'NONE',  ( 0.000000000000000000, 0.000000000000000000, 1.000000000000000000 ) ) ;
#6071=EDGE_CURVE ( 'NONE', #4594, #997, #5356, .T. ) ;
#6073=ORIENTED_EDGE ( 'NONE', *, *, #7851, .T. ) ;
#6076=CARTESIAN_POINT ( 'NONE',  ( 4.999999999999999112, -22.37914155802287297, 2.791921004064167544 ) ) ;
#6080=DIRECTION ( 'NONE',  ( 0.000000000000000000, 0.9238795325112877377, -0.3826834323650873393 ) ) ;
#6081=CARTESIAN_POINT ( 'NONE',  ( 0.000000000000000000, 0.000000000000000000, 0.000000000000000000 ) ) ;
#6085=CARTESIAN_POINT ( 'NONE',  ( 4.999999999999999112, 13.17168466712928598, 15.37949036966216632 ) ) ;
#6086=ORIENTED_EDGE ( 'NONE', *, *, #8612, .T. ) ;
#6088=EDGE_CURVE ( 'NONE', #9230, #6352, #6419, .T. ) ;
#6090=CARTESIAN_POINT ( 'NONE',  ( 0.000000000000000000, 15.37949036966211835, 13.17168466712934105 ) ) ;
#6095=DIRECTION ( 'NONE',  ( 0.000000000000000000, -1.000000000000000000, -1.048062100068272767E-14 ) ) ;
#6099=DIRECTION ( 'NONE',  ( 0.000000000000000000, 0.000000000000000000, 1.000000000000000000 ) ) ;
#6107=CARTESIAN_POINT ( 'NONE',  ( 2.499999999999999556, 14.41081992069341133, -22.83261415639488234 ) ) ;
#6109=CARTESIAN_POINT ( 'NONE',  ( 0.000000000000000000, 0.000000000000000000, 0.000000000000000000 ) ) ;
#6115=ORIENTED_EDGE ( 'NONE', *, *, #5554, .F. ) ;
#6121=DIRECTION ( 'NONE',  ( 0.000000000000000000, -0.7071067811865536790, 0.7071067811865413555 ) ) ;
#6124=CARTESIAN_POINT ( 'NONE',  ( 4.999999999999999112, 0.000000000000000000, 0.000000000000000000 ) ) ;
#6125=VERTEX_POINT ( 'NONE', #6423 ) ;
#6136=DIRECTION ( 'NONE',  ( -1.000000000000000000, 0.000000000000000000, 0.000000000000000000 ) ) ;
#6157=CARTESIAN_POINT ( 'NONE',  ( 0.000000000000000000, -22.83261415639492498, -14.41081992069334561 ) ) ;
#6167=ORIENTED_EDGE ( 'NONE', *, *, #10800, .T. ) ;
#6171=CARTESIAN_POINT ( 'NONE',  ( 4.999999999999999112, -19.60720892790260805, 11.14352537685167732 ) ) ;
#6175=PLANE ( 'NONE',  #7607 ) ;
#6178=AXIS2_PLACEMENT_3D ( 'NONE', #10174, #7369, #10297 ) ;
#6180=CIRCLE ( 'NONE', #582, 9.600000000009599077 ) ;
#6184=DIRECTION ( 'NONE',  ( 0.000000000000000000, 0.000000000000000000, 1.000000000000000000 ) ) ;
#6185=ORIENTED_EDGE ( 'NONE', *, *, #9742, .T. ) ;
#6187=CIRCLE ( 'NONE', #2194, 9.600000000009600853 ) ;
#6189=CIRCLE ( 'NONE', #3391, 9.600000000009600853 ) ;
#6194=CARTESIAN_POINT ( 'NONE',  ( 4.999999999999997335, 0.000000000000000000, 0.000000000000000000 ) ) ;
#6196=VECTOR ( 'NONE', #700, 1000.000000000000000 ) ;
#6197=ORIENTED_EDGE ( 'NONE', *, *, #174, .T. ) ;
#6215=DIRECTION ( 'NONE',  ( -1.000000000000000000, 0.000000000000000000, 0.000000000000000000 ) ) ;
#6218=DIRECTION ( 'NONE',  ( 0.000000000000000000, 0.000000000000000000, -1.000000000000000000 ) ) ;
#6221=CIRCLE ( 'NONE', #6830, 9.600000000009600853 ) ;
#6228=FACE_OUTER_BOUND ( 'NONE', #5265, .T. ) ;
#6233=DIRECTION ( 'NONE',  ( 0.000000000000000000, 0.000000000000000000, -1.000000000000000000 ) ) ;
#6238=VERTEX_POINT ( 'NONE', #10711 ) ;
#6239=VECTOR ( 'NONE', #10400, 1000.000000000000000 ) ;
#6247=EDGE_CURVE ( 'NONE', #9598, #1449, #7639, .T. ) ;
#6253=CIRCLE ( 'NONE', #10438, 9.600000000009602630 ) ;
#6258=ORIENTED_EDGE ( 'NONE', *, *, #7159, .F. ) ;
#6261=EDGE_CURVE ( 'NONE', #8991, #3326, #1461, .T. ) ;
#6263=LINE ( 'NONE', #7134, #404 ) ;
#6266=VERTEX_POINT ( 'NONE', #9906 ) ;
#6279=ORIENTED_EDGE ( 'NONE', *, *, #9761, .T. ) ;
#6280=CARTESIAN_POINT ( 'NONE',  ( 4.999999999999999112, 9.168210874537823685, -18.05452603534156353 ) ) ;
#6286=CARTESIAN_POINT ( 'NONE',  ( 0.000000000000000000, 6.799999999999999822, 1.500000000000000000 ) ) ;
#6305=CIRCLE ( 'NONE', #4291, 9.600000000009602630 ) ;
#6313=EDGE_CURVE ( 'NONE', #9964, #1066, #834, .T. ) ;
#6314=ADVANCED_FACE ( 'NONE', ( #10023 ), #2271, .T. ) ;
#6318=CARTESIAN_POINT ( 'NONE',  ( 4.999999999999999112, 0.000000000000000000, 0.000000000000000000 ) ) ;
#6321=DIRECTION ( 'NONE',  ( 0.000000000000000000, 0.000000000000000000, 1.000000000000000000 ) ) ;
#6322=VERTEX_POINT ( 'NONE', #6090 ) ;
#6323=EDGE_LOOP ( 'NONE', ( #5635, #8311, #1537, #11840 ) ) ;
#6324=DIRECTION ( 'NONE',  ( 0.000000000000000000, -0.9238795325112906243, 0.3826834323650805669 ) ) ;
#6335=ADVANCED_FACE ( 'NONE', ( #4140 ), #5275, .T. ) ;
#6337=CARTESIAN_POINT ( 'NONE',  ( 0.000000000000000000, -19.24938187143291657, -6.283573709965514453 ) ) ;
#6343=CYLINDRICAL_SURFACE ( 'NONE', #7892, 9.600000000009600853 ) ;
#6344=ORIENTED_EDGE ( 'NONE', *, *, #2537, .F. ) ;
#6346=CARTESIAN_POINT ( 'NONE',  ( 4.999999999999999112, 18.05452603534179090, -9.168210874537381372 ) ) ;
#6350=ORIENTED_EDGE ( 'NONE', *, *, #6986, .F. ) ;
#6352=VERTEX_POINT ( 'NONE', #3517 ) ;
#6363=AXIS2_PLACEMENT_3D ( 'NONE', #7125, #2355, #6121 ) ;
#6367=FACE_OUTER_BOUND ( 'NONE', #7025, .T. ) ;
#6370=CIRCLE ( 'NONE', #6786, 27.00000000002699707 ) ;
#6373=AXIS2_PLACEMENT_3D ( 'NONE', #4401, #526, #10961 ) ;
#6383=ORIENTED_EDGE ( 'NONE', *, *, #9722, .F. ) ;
#6386=ORIENTED_EDGE ( 'NONE', *, *, #7106, .F. ) ;
#6396=CIRCLE ( 'NONE', #2596, 27.00000000002699707 ) ;
#6397=DIRECTION ( 'NONE',  ( 0.000000000000000000, 0.000000000000000000, 1.000000000000000000 ) ) ;
#6398=CARTESIAN_POINT ( 'NONE',  ( 4.999999999999999112, 0.000000000000000000, 0.000000000000000000 ) ) ;
#6402=ORIENTED_EDGE ( 'NONE', *, *, #3717, .F. ) ;
#6404=VERTEX_POINT ( 'NONE', #7283 ) ;
#6407=VECTOR ( 'NONE', #8837, 1000.000000000000000 ) ;
#6411=CARTESIAN_POINT ( 'NONE',  ( 2.500000000000000444, -5.955107813822308138, -26.33508479058327367 ) ) ;
#6419=CIRCLE ( 'NONE', #1022, 9.600000000009600853 ) ;
#6423=CARTESIAN_POINT ( 'NONE',  ( 4.999999999999999112, -9.168210874537708222, 18.05452603534162748 ) ) ;
#6427=CIRCLE ( 'NONE', #2425, 27.00000000002699707 ) ;
#6430=AXIS2_PLACEMENT_3D ( 'NONE', #1601, #3420, #5425 ) ;
#6444=VECTOR ( 'NONE', #3287, 1000.000000000000000 ) ;
#6447=VECTOR ( 'NONE', #3202, 1000.000000000000000 ) ;
#6459=VECTOR ( 'NONE', #5561, 1000.000000000000000 ) ;
#6461=CARTESIAN_POINT ( 'NONE',  ( 2.499999999999999556, -22.83261415639492498, -14.41081992069334383 ) ) ;
#6465=ORIENTED_EDGE ( 'NONE', *, *, #1520, .F. ) ;
#6467=DIRECTION ( 'NONE',  ( -1.000000000000000000, -0.000000000000000000, -0.000000000000000000 ) ) ;
#6471=LINE ( 'NONE', #4463, #3027 ) ;
#6472=ORIENTED_EDGE ( 'NONE', *, *, #10286, .F. ) ;
#6480=DIRECTION ( 'NONE',  ( -1.000000000000000000, 0.000000000000000000, 0.000000000000000000 ) ) ;
#6482=CARTESIAN_POINT ( 'NONE',  ( 4.999999999999999112, 20.18872947935930995, -1.561154383803291967 ) ) ;
#6486=LINE ( 'NONE', #772, #852 ) ;
#6489=ORIENTED_EDGE ( 'NONE', *, *, #1732, .F. ) ;
#6495=DIRECTION ( 'NONE',  ( -1.000000000000000000, 0.000000000000000000, 0.000000000000000000 ) ) ;
#6498=EDGE_CURVE ( 'NONE', #8156, #7335, #9211, .T. ) ;
#6501=VERTEX_POINT ( 'NONE', #7649 ) ;
#6502=AXIS2_PLACEMENT_3D ( 'NONE', #2627, #509, #8277 ) ;
#6506=DIRECTION ( 'NONE',  ( -1.000000000000000000, -0.000000000000000000, 0.000000000000000000 ) ) ;
#6510=ORIENTED_EDGE ( 'NONE', *, *, #11271, .F. ) ;
#6541=ORIENTED_EDGE ( 'NONE', *, *, #6933, .F. ) ;
#6551=VERTEX_POINT ( 'NONE', #3701 ) ;
#6553=ORIENTED_EDGE ( 'NONE', *, *, #10193, .F. ) ;
#6555=ORIENTED_EDGE ( 'NONE', *, *, #1100, .T. ) ;
#6556=LINE ( 'NONE', #3745, #7370 ) ;
#6557=EDGE_CURVE ( 'NONE', #1857, #3502, #11373, .T. ) ;
#6564=CARTESIAN_POINT ( 'NONE',  ( 0.000000000000000000, -15.57980286237488343, 22.05152472667124997 ) ) ;
#6570=CARTESIAN_POINT ( 'NONE',  ( 4.999999999999999112, -5.984728032764810024, -21.74405275335764287 ) ) ;
#6576=CARTESIAN_POINT ( 'NONE',  ( 0.000000000000000000, 0.000000000000000000, 1.500000000000000000 ) ) ;
#6579=DIRECTION ( 'NONE',  ( -1.000000000000000000, -0.000000000000000000, -0.000000000000000000 ) ) ;
#6590=VECTOR ( 'NONE', #3166, 1000.000000000000000 ) ;
#6600=AXIS2_PLACEMENT_3D ( 'NONE', #8593, #3100, #7671 ) ;
#6601=ORIENTED_EDGE ( 'NONE', *, *, #414, .F. ) ;
#6606=ORIENTED_EDGE ( 'NONE', *, *, #5750, .F. ) ;
#6610=CARTESIAN_POINT ( 'NONE',  ( 0.000000000000000000, 14.41081992069341133, -22.83261415639488234 ) ) ;
#6619=ORIENTED_EDGE ( 'NONE', *, *, #3902, .T. ) ;
#6621=EDGE_LOOP ( 'NONE', ( #11128, #3114, #9914, #9467 ) ) ;
#6628=PRODUCT ( 'spur gear_iso_ISO - Spur gear 3M 16T 20PA 5FW ---S16A75H50L10.0S1', 'spur gear_iso_ISO - Spur gear 3M 16T 20PA 5FW ---S16A75H50L10.0S1', '', ( #3728 ) ) ;
#6633=DIRECTION ( 'NONE',  ( 1.000000000000000000, -0.000000000000000000, -0.000000000000000000 ) ) ;
#6638=AXIS2_PLACEMENT_3D ( 'NONE', #3721, #7534, #4472 ) ;
#6639=VECTOR ( 'NONE', #1563, 1000.000000000000000 ) ;
#6644=ORIENTED_EDGE ( 'NONE', *, *, #3771, .F. ) ;
#6648=DIRECTION ( 'NONE',  ( -1.000000000000000000, 0.000000000000000000, -0.000000000000000000 ) ) ;
#6649=EDGE_LOOP ( 'NONE', ( #3239, #2111, #5064, #5471 ) ) ;
#6652=CIRCLE ( 'NONE', #1241, 5.000000000000000000 ) ;
#6655=CARTESIAN_POINT ( 'NONE',  ( 4.999999999999999112, -19.24938187143291657, -6.283573709965514453 ) ) ;
#6658=AXIS2_PLACEMENT_3D ( 'NONE', #3089, #2133, #11447 ) ;
#6672=DIRECTION ( 'NONE',  ( -1.000000000000000000, 0.000000000000000000, -0.000000000000000000 ) ) ;
#6675=ORIENTED_EDGE ( 'NONE', *, *, #4167, .T. ) ;
#6676=DIRECTION ( 'NONE',  ( 0.000000000000000000, 0.000000000000000000, 1.000000000000000000 ) ) ;
#6688=AXIS2_PLACEMENT_3D ( 'NONE', #7603, #6793, #7679 ) ;
#6691=EDGE_CURVE ( 'NONE', #7692, #5247, #8082, .T. ) ;
#6697=CIRCLE ( 'NONE', #3098, 9.600000000009600853 ) ;
#6704=CARTESIAN_POINT ( 'NONE',  ( 50.00005079999999680, 6.799999999999999822, 1.500000000000000000 ) ) ;
#6705=DIRECTION ( 'NONE',  ( -1.000000000000000000, -0.000000000000000000, -0.000000000000000000 ) ) ;
#6706=ADVANCED_FACE ( 'NONE', ( #186 ), #1252, .T. ) ;
#6713=VECTOR ( 'NONE', #9319, 1000.000000000000000 ) ;
#6722=CARTESIAN_POINT ( 'NONE',  ( 4.999999999999999112, -18.05452603534159195, -9.168210874537770394 ) ) ;
#6723=DIRECTION ( 'NONE',  ( 0.000000000000000000, 0.7071067811865487940, -0.7071067811865462405 ) ) ;
#6733=ORIENTED_EDGE ( 'NONE', *, *, #10447, .F. ) ;
#6741=ORIENTED_EDGE ( 'NONE', *, *, #5934, .T. ) ;
#6742=CARTESIAN_POINT ( 'NONE',  ( -10.00000000000000000, 0.000000000000000000, 0.000000000000000000 ) ) ;
#6745=CARTESIAN_POINT ( 'NONE',  ( 0.000000000000000000, -19.60720892790260805, 11.14352537685167732 ) ) ;
#6746=ORIENTED_EDGE ( 'NONE', *, *, #6813, .T. ) ;
#6748=ORIENTED_EDGE ( 'NONE', *, *, #2634, .F. ) ;
#6752=CARTESIAN_POINT ( 'NONE',  ( 4.999999999999999112, -19.60720892790245529, -11.14352537685195266 ) ) ;
#6758=DIRECTION ( 'NONE',  ( -1.000000000000000000, 0.000000000000000000, 0.000000000000000000 ) ) ;
#6775=FACE_OUTER_BOUND ( 'NONE', #2473, .T. ) ;
#6776=UNCERTAINTY_MEASURE_WITH_UNIT (LENGTH_MEASURE( 1.000000000000000082E-05 ), #636, 'distance_accuracy_value', 'NONE');
#6777=CIRCLE ( 'NONE', #4163, 5.000000000000000000 ) ;
#6779=ORIENTED_EDGE ( 'NONE', *, *, #9163, .T. ) ;
#6784=CARTESIAN_POINT ( 'NONE',  ( 0.000000000000000000, 4.576198416197252428, 26.60936692326691499 ) ) ;
#6786=AXIS2_PLACEMENT_3D ( 'NONE', #2110, #3397, #7807 ) ;
#6788=DIRECTION ( 'NONE',  ( -1.000000000000000000, -0.000000000000000000, -0.000000000000000000 ) ) ;
#6790=ORIENTED_EDGE ( 'NONE', *, *, #3933, .F. ) ;
#6792=ORIENTED_EDGE ( 'NONE', *, *, #8994, .F. ) ;
#6793=DIRECTION ( 'NONE',  ( 1.000000000000000000, 0.000000000000000000, 0.000000000000000000 ) ) ;
#6795=ORIENTED_EDGE ( 'NONE', *, *, #5408, .T. ) ;
#6803=CARTESIAN_POINT ( 'NONE',  ( 0.000000000000000000, 0.000000000000000000, 0.000000000000000000 ) ) ;
#6812=ORIENTED_EDGE ( 'NONE', *, *, #4195, .F. ) ;
#6813=EDGE_CURVE ( 'NONE', #5310, #978, #10572, .T. ) ;
#6820=DIRECTION ( 'NONE',  ( -1.000000000000000000, 0.000000000000000000, -0.000000000000000000 ) ) ;
#6823=CARTESIAN_POINT ( 'NONE',  ( 4.999999999999999112, -6.283573709965446064, 19.24938187143294144 ) ) ;
#6830=AXIS2_PLACEMENT_3D ( 'NONE', #3406, #584, #11150 ) ;
#6832=DIRECTION ( 'NONE',  ( -1.000000000000000000, 0.000000000000000000, 0.000000000000000000 ) ) ;
#6837=AXIS2_PLACEMENT_3D ( 'NONE', #1914, #10588, #9597 ) ;
#6839=FACE_OUTER_BOUND ( 'NONE', #2976, .T. ) ;
#6844=ORIENTED_EDGE ( 'NONE', *, *, #60, .T. ) ;
#6845=EDGE_CURVE ( 'NONE', #10053, #8252, #580, .T. ) ;
#6849=VERTEX_POINT ( 'NONE', #7443 ) ;
#6850=CYLINDRICAL_SURFACE ( 'NONE', #4882, 5.000000000000000000 ) ;
#6852=VECTOR ( 'NONE', #1082, 1000.000000000000000 ) ;
#6863=ADVANCED_FACE ( 'NONE', ( #2431 ), #2544, .T. ) ;
#6864=EDGE_CURVE ( 'NONE', #5720, #7438, #12156, .T. ) ;
#6867=CIRCLE ( 'NONE', #4449, 20.24900000002024569 ) ;
#6868=AXIS2_PLACEMENT_3D ( 'NONE', #3511, #2504, #555 ) ;
#6869=LINE ( 'NONE', #9972, #11162 ) ;
#6872=CARTESIAN_POINT ( 'NONE',  ( 0.000000000000000000, -14.41081992069293349, -22.83261415639518432 ) ) ;
#6874=DIRECTION ( 'NONE',  ( -1.000000000000000000, 0.000000000000000000, 0.000000000000000000 ) ) ;
#6875=VERTEX_POINT ( 'NONE', #4553 ) ;
#6881=ORIENTED_EDGE ( 'NONE', *, *, #10154, .T. ) ;
#6883=ORIENTED_EDGE ( 'NONE', *, *, #6313, .T. ) ;
#6887=EDGE_CURVE ( 'NONE', #7155, #4621, #1387, .T. ) ;
#6890=LINE ( 'NONE', #8942, #2654 ) ;
#6898=DIRECTION ( 'NONE',  ( -1.000000000000000000, 0.000000000000000000, 0.000000000000000000 ) ) ;
#6904=VERTEX_POINT ( 'NONE', #8264 ) ;
#6907=EDGE_LOOP ( 'NONE', ( #12035, #11104, #11879, #8869 ) ) ;
#6908=DIRECTION ( 'NONE',  ( 0.000000000000000000, 0.3826834323650841752, 0.9238795325112890700 ) ) ;
#6910=ORIENTED_EDGE ( 'NONE', *, *, #414, .T. ) ;
#6922=EDGE_CURVE ( 'NONE', #9598, #6404, #11172, .T. ) ;
#6925=DIRECTION ( 'NONE',  ( 0.000000000000000000, 0.000000000000000000, 1.000000000000000000 ) ) ;
#6927=DIRECTION ( 'NONE',  ( -1.000000000000000000, -0.000000000000000000, -0.000000000000000000 ) ) ;
#6933=EDGE_CURVE ( 'NONE', #5247, #9896, #10772, .T. ) ;
#6936=ADVANCED_FACE ( 'NONE', ( #6367 ), #9321, .T. ) ;
#6938=ADVANCED_FACE ( 'NONE', ( #7266 ), #5256, .T. ) ;
#6944=DIRECTION ( 'NONE',  ( -1.000000000000000000, 0.000000000000000000, 0.000000000000000000 ) ) ;
#6952=CARTESIAN_POINT ( 'NONE',  ( 4.999999999999999112, 20.18872947935930995, -1.561154383803291967 ) ) ;
#6957=ORIENTED_EDGE ( 'NONE', *, *, #463, .F. ) ;
#6961=DIRECTION ( 'NONE',  ( -1.000000000000000000, 0.000000000000000000, 0.000000000000000000 ) ) ;
#6966=FACE_OUTER_BOUND ( 'NONE', #7939, .T. ) ;
#6972=EDGE_LOOP ( 'NONE', ( #1989, #48, #3474, #11312 ) ) ;
#6984=ORIENTED_EDGE ( 'NONE', *, *, #3947, .T. ) ;
#6986=EDGE_CURVE ( 'NONE', #3187, #4264, #563, .T. ) ;
#6987=ORIENTED_EDGE ( 'NONE', *, *, #4930, .F. ) ;
#6988=CIRCLE ( 'NONE', #190, 27.00000000002699707 ) ;
#6990=CARTESIAN_POINT ( 'NONE',  ( 0.000000000000000000, 0.000000000000000000, 0.000000000000000000 ) ) ;
#6995=ORIENTED_EDGE ( 'NONE', *, *, #148, .F. ) ;
#6998=VERTEX_POINT ( 'NONE', #5553 ) ;
#6999=CARTESIAN_POINT ( 'NONE',  ( 0.000000000000000000, -26.33508479058324880, 5.955107813822411167 ) ) ;
#7000=EDGE_CURVE ( 'NONE', #2800, #4492, #6556, .T. ) ;
#7006=ORIENTED_EDGE ( 'NONE', *, *, #8852, .F. ) ;
#7011=AXIS2_PLACEMENT_3D ( 'NONE', #2894, #9713, #7578 ) ;
#7013=FACE_OUTER_BOUND ( 'NONE', #9320, .T. ) ;
#7014=AXIS2_PLACEMENT_3D ( 'NONE', #8927, #7982, #6233 ) ;
#7015=VECTOR ( 'NONE', #11474, 1000.000000000000000 ) ;
#7018=ORIENTED_EDGE ( 'NONE', *, *, #8398, .T. ) ;
#7020=CARTESIAN_POINT ( 'NONE',  ( 0.000000000000000000, 26.60936692326690789, 4.576198416197345686 ) ) ;
#7021=DIRECTION ( 'NONE',  ( -1.000000000000000000, -0.000000000000000000, 0.000000000000000000 ) ) ;
#7025=EDGE_LOOP ( 'NONE', ( #10650, #12020, #4204, #180 ) ) ;
#7030=AXIS2_PLACEMENT_3D ( 'NONE', #4143, #8915, #2146 ) ;
#7032=DIRECTION ( 'NONE',  ( 0.000000000000000000, 0.000000000000000000, 1.000000000000000000 ) ) ;
#7042=VERTEX_POINT ( 'NONE', #11358 ) ;
#7047=AXIS2_PLACEMENT_3D ( 'NONE', #3315, #3137, #7071 ) ;
#7052=CARTESIAN_POINT ( 'NONE',  ( 50.00005079999999680, 0.000000000000000000, 5.000000000000000000 ) ) ;
#7053=CARTESIAN_POINT ( 'NONE',  ( 4.999999999999999112, -13.17168466712939257, 15.37949036966207039 ) ) ;
#7067=CARTESIAN_POINT ( 'NONE',  ( 4.999999999999999112, 22.05152472667129970, 15.57980286237480350 ) ) ;
#7068=ORIENTED_EDGE ( 'NONE', *, *, #9209, .F. ) ;
#7071=DIRECTION ( 'NONE',  ( 0.000000000000000000, 0.9238795325112850731, 0.3826834323650936676 ) ) ;
#7074=ORIENTED_EDGE ( 'NONE', *, *, #4773, .F. ) ;
#7075=DIRECTION ( 'NONE',  ( -1.000000000000000000, -0.000000000000000000, 0.000000000000000000 ) ) ;
#7081=CARTESIAN_POINT ( 'NONE',  ( 4.999999999999999112, -13.17168466712917585, -15.37949036966225513 ) ) ;
#7089=ORIENTED_EDGE ( 'NONE', *, *, #965, .F. ) ;
#7092=DIRECTION ( 'NONE',  ( 0.000000000000000000, 0.000000000000000000, 1.000000000000000000 ) ) ;
#7093=CIRCLE ( 'NONE', #12057, 20.24900000002024569 ) ;
#7097=CARTESIAN_POINT ( 'NONE',  ( -10.00000000000000000, 0.000000000000000000, 0.000000000000000000 ) ) ;
#7099=DIRECTION ( 'NONE',  ( 0.000000000000000000, 0.7071067811865486830, -0.7071067811865464625 ) ) ;
#7101=CIRCLE ( 'NONE', #6502, 20.24900000002024569 ) ;
#7102=CARTESIAN_POINT ( 'NONE',  ( 4.999999999999999112, 4.576198416197251539, 26.60936692326691855 ) ) ;
#7106=EDGE_CURVE ( 'NONE', #12088, #10665, #11339, .T. ) ;
#7107=EDGE_CURVE ( 'NONE', #1798, #1083, #11537, .T. ) ;
#7110=DIRECTION ( 'NONE',  ( 0.000000000000000000, -0.3826834323650971648, 0.9238795325112837409 ) ) ;
#7114=ORIENTED_EDGE ( 'NONE', *, *, #9531, .F. ) ;
#7119=LINE ( 'NONE', #9931, #8630 ) ;
#7122=ORIENTED_EDGE ( 'NONE', *, *, #3296, .F. ) ;
#7125=CARTESIAN_POINT ( 'NONE',  ( 0.000000000000000000, -21.74405275335753984, -5.984728032765188388 ) ) ;
#7131=APPLICATION_CONTEXT ( 'automotive_design' ) ;
#7134=CARTESIAN_POINT ( 'NONE',  ( 4.999999999999999112, 6.283573709965571297, -19.24938187143289881 ) ) ;
#7135=DIRECTION ( 'NONE',  ( 0.000000000000000000, 0.000000000000000000, 1.000000000000000000 ) ) ;
#7141=DIRECTION ( 'NONE',  ( 0.000000000000000000, -0.3826834323650773473, -0.9238795325112919565 ) ) ;
#7151=ORIENTED_EDGE ( 'NONE', *, *, #3739, .T. ) ;
#7155=VERTEX_POINT ( 'NONE', #5112 ) ;
#7157=EDGE_CURVE ( 'NONE', #2328, #5671, #2991, .T. ) ;
#7159=EDGE_CURVE ( 'NONE', #6849, #8668, #4161, .T. ) ;
#7161=EDGE_CURVE ( 'NONE', #3985, #3572, #4961, .T. ) ;
#7162=LINE ( 'NONE', #3404, #4774 ) ;
#7164=DIRECTION ( 'NONE',  ( -1.000000000000000000, -0.000000000000000000, 0.000000000000000000 ) ) ;
#7169=DIRECTION ( 'NONE',  ( 0.000000000000000000, 1.000000000000000000, 3.614007241614734605E-15 ) ) ;
#7173=EDGE_LOOP ( 'NONE', ( #6402, #234, #3318, #11096 ) ) ;
#7178=CIRCLE ( 'NONE', #5374, 27.00000000002699707 ) ;
#7185=ADVANCED_FACE ( 'NONE', ( #1118 ), #9878, .T. ) ;
#7192=DIRECTION ( 'NONE',  ( 0.000000000000000000, 0.000000000000000000, 1.000000000000000000 ) ) ;
#7198=DIRECTION ( 'NONE',  ( 0.000000000000000000, 0.000000000000000000, -1.000000000000000000 ) ) ;
#7205=AXIS2_PLACEMENT_3D ( 'NONE', #930, #6820, #1120 ) ;
#7212=ORIENTED_EDGE ( 'NONE', *, *, #6088, .F. ) ;
#7215=CARTESIAN_POINT ( 'NONE',  ( 0.000000000000000000, 0.000000000000000000, 0.000000000000000000 ) ) ;
#7219=DIRECTION ( 'NONE',  ( -1.000000000000000000, -0.000000000000000000, -0.000000000000000000 ) ) ;
#7220=VERTEX_POINT ( 'NONE', #4928 ) ;
#7223=AXIS2_PLACEMENT_3D ( 'NONE', #3537, #5593, #4668 ) ;
#7236=CARTESIAN_POINT ( 'NONE',  ( 4.999999999999999112, 0.000000000000000000, 0.000000000000000000 ) ) ;
#7238=AXIS2_PLACEMENT_3D ( 'NONE', #7787, #9483, #11578 ) ;
#7239=AXIS2_PLACEMENT_3D ( 'NONE', #4197, #7962, #7092 ) ;
#7248=( GEOMETRIC_REPRESENTATION_CONTEXT ( 3 ) GLOBAL_UNCERTAINTY_ASSIGNED_CONTEXT ( ( #11388 ) ) GLOBAL_UNIT_ASSIGNED_CONTEXT ( ( #12161, #10545, #985 ) ) REPRESENTATION_CONTEXT ( 'NONE', 'WORKASPACE' ) );
#7255=ORIENTED_EDGE ( 'NONE', *, *, #9786, .F. ) ;
#7259=AXIS2_PLACEMENT_3D ( 'NONE', #1780, #9417, #6676 ) ;
#7264=DIRECTION ( 'NONE',  ( -1.000000000000000000, 0.000000000000000000, 0.000000000000000000 ) ) ;
#7266=FACE_OUTER_BOUND ( 'NONE', #1726, .T. ) ;
#7268=CIRCLE ( 'NONE', #4062, 9.600000000009600853 ) ;
#7272=FACE_OUTER_BOUND ( 'NONE', #253, .T. ) ;
#7274=CARTESIAN_POINT ( 'NONE',  ( 4.999999999999999112, -22.05152472667118957, -15.57980286237495626 ) ) ;
#7276=ORIENTED_EDGE ( 'NONE', *, *, #3250, .T. ) ;
#7283=CARTESIAN_POINT ( 'NONE',  ( 0.000000000000000000, 9.168210874537578547, 18.05452603534168787 ) ) ;
#7284=VECTOR ( 'NONE', #4852, 1000.000000000000000 ) ;
#7299=LINE ( 'NONE', #4338, #5822 ) ;
#7301=PLANE ( 'NONE',  #422 ) ;
#7302=CYLINDRICAL_SURFACE ( 'NONE', #4034, 20.24900000002024569 ) ;
#7303=ORIENTED_EDGE ( 'NONE', *, *, #2613, .F. ) ;
#7304=CYLINDRICAL_SURFACE ( 'NONE', #453, 9.600000000009600853 ) ;
#7314=DIRECTION ( 'NONE',  ( 0.000000000000000000, 0.000000000000000000, 1.000000000000000000 ) ) ;
#7315=ORIENTED_EDGE ( 'NONE', *, *, #343, .F. ) ;
#7319=ORIENTED_EDGE ( 'NONE', *, *, #11638, .T. ) ;
#7323=ORIENTED_EDGE ( 'NONE', *, *, #4876, .T. ) ;
#7335=VERTEX_POINT ( 'NONE', #673 ) ;
#7337=ORIENTED_EDGE ( 'NONE', *, *, #3118, .F. ) ;
#7343=ORIENTED_EDGE ( 'NONE', *, *, #8147, .T. ) ;
#7349=CARTESIAN_POINT ( 'NONE',  ( 0.000000000000000000, 6.123233995736766282E-16, -5.000000000000000000 ) ) ;
#7351=FACE_OUTER_BOUND ( 'NONE', #12060, .T. ) ;
#7356=ORIENTED_EDGE ( 'NONE', *, *, #5995, .T. ) ;
#7359=ORIENTED_EDGE ( 'NONE', *, *, #10243, .F. ) ;
#7366=ADVANCED_FACE ( 'NONE', ( #11161 ), #3490, .T. ) ;
#7369=DIRECTION ( 'NONE',  ( 1.000000000000000000, 0.000000000000000000, 0.000000000000000000 ) ) ;
#7370=VECTOR ( 'NONE', #6633, 1000.000000000000000 ) ;
#7377=VECTOR ( 'NONE', #8500, 1000.000000000000000 ) ;
#7386=ORIENTED_EDGE ( 'NONE', *, *, #4487, .T. ) ;
#7388=DIRECTION ( 'NONE',  ( 0.000000000000000000, 0.000000000000000000, 1.000000000000000000 ) ) ;
#7389=CIRCLE ( 'NONE', #8387, 9.600000000009599077 ) ;
#7398=EDGE_LOOP ( 'NONE', ( #2560, #8539, #7303, #1336 ) ) ;
#7411=ADVANCED_FACE ( 'NONE', ( #4729 ), #5672, .T. ) ;
#7413=CYLINDRICAL_SURFACE ( 'NONE', #11195, 20.24900000002024569 ) ;
#7415=CARTESIAN_POINT ( 'NONE',  ( 0.000000000000000000, -5.984728032764810024, -21.74405275335764287 ) ) ;
#7421=LINE ( 'NONE', #1722, #64 ) ;
#7423=ORIENTED_EDGE ( 'NONE', *, *, #4875, .F. ) ;
#7435=VERTEX_POINT ( 'NONE', #3608 ) ;
#7438=VERTEX_POINT ( 'NONE', #6610 ) ;
#7443=CARTESIAN_POINT ( 'NONE',  ( 4.999999999999999112, -5.955107813822311691, -26.33508479058326657 ) ) ;
#7445=ADVANCED_FACE ( 'NONE', ( #915 ), #10412, .T. ) ;
#7447=AXIS2_PLACEMENT_3D ( 'NONE', #12189, #10386, #9217 ) ;
#7450=DIRECTION ( 'NONE',  ( -1.000000000000000000, -0.000000000000000000, 0.000000000000000000 ) ) ;
#7460=VERTEX_POINT ( 'NONE', #3732 ) ;
#7462=EDGE_CURVE ( 'NONE', #8252, #11705, #982, .T. ) ;
#7466=ORIENTED_EDGE ( 'NONE', *, *, #4148, .F. ) ;
#7469=ORIENTED_EDGE ( 'NONE', *, *, #119, .F. ) ;
#7477=EDGE_CURVE ( 'NONE', #12254, #2589, #12150, .T. ) ;
#7481=DIRECTION ( 'NONE',  ( -1.000000000000000000, 0.000000000000000000, 0.000000000000000000 ) ) ;
#7494=DIRECTION ( 'NONE',  ( 0.000000000000000000, 0.000000000000000000, 1.000000000000000000 ) ) ;
#7495=VECTOR ( 'NONE', #4940, 1000.000000000000000 ) ;
#7507=CARTESIAN_POINT ( 'NONE',  ( 4.999999999999999112, 4.576198416197620134, -26.60936692326685460 ) ) ;
#7521=DIRECTION ( 'NONE',  ( -1.000000000000000000, -0.000000000000000000, -0.000000000000000000 ) ) ;
#7523=ORIENTED_EDGE ( 'NONE', *, *, #9163, .F. ) ;
#7524=ADVANCED_FACE ( 'NONE', ( #11085 ), #10206, .T. ) ;
#7526=CARTESIAN_POINT ( 'NONE',  ( 0.000000000000000000, 0.000000000000000000, 0.000000000000000000 ) ) ;
#7531=DIRECTION ( 'NONE',  ( 0.000000000000000000, 0.000000000000000000, 1.000000000000000000 ) ) ;
#7534=DIRECTION ( 'NONE',  ( -1.000000000000000000, -0.000000000000000000, 0.000000000000000000 ) ) ;
#7535=DIRECTION ( 'NONE',  ( -1.000000000000000000, -0.000000000000000000, -0.000000000000000000 ) ) ;
#7544=EDGE_LOOP ( 'NONE', ( #6541, #1884, #1982, #9352 ) ) ;
#7553=CARTESIAN_POINT ( 'NONE',  ( 4.999999999999999112, 0.000000000000000000, 0.000000000000000000 ) ) ;
#7561=CARTESIAN_POINT ( 'NONE',  ( 4.999999999999999112, -19.60720892790260805, 11.14352537685167732 ) ) ;
#7568=CARTESIAN_POINT ( 'NONE',  ( 2.499999999999999556, -26.60936692326687592, -4.576198416197529539 ) ) ;
#7570=VERTEX_POINT ( 'NONE', #11204 ) ;
#7578=DIRECTION ( 'NONE',  ( 0.000000000000000000, 0.000000000000000000, 1.000000000000000000 ) ) ;
#7588=ORIENTED_EDGE ( 'NONE', *, *, #5846, .T. ) ;
#7595=CARTESIAN_POINT ( 'NONE',  ( 4.999999999999999112, -21.74405275335762155, 15.58472803277448726 ) ) ;
#7603=CARTESIAN_POINT ( 'NONE',  ( 0.000000000000000000, 2.791921004064568113, -22.37914155802282323 ) ) ;
#7607=AXIS2_PLACEMENT_3D ( 'NONE', #9814, #3249, #5113 ) ;
#7610=DIRECTION ( 'NONE',  ( -1.000000000000000000, 0.000000000000000000, -0.000000000000000000 ) ) ;
#7618=CIRCLE ( 'NONE', #9416, 9.600000000009599077 ) ;
#7634=ADVANCED_FACE ( 'NONE', ( #1762 ), #12258, .T. ) ;
#7637=CIRCLE ( 'NONE', #4428, 27.00000000002699707 ) ;
#7638=AXIS2_PLACEMENT_3D ( 'NONE', #10159, #12273, #11040 ) ;
#7639=CIRCLE ( 'NONE', #41, 9.600000000009600853 ) ;
#7640=CARTESIAN_POINT ( 'NONE',  ( 0.000000000000000000, -26.60936692326693631, 4.576198416197160057 ) ) ;
#7642=VERTEX_POINT ( 'NONE', #9400 ) ;
#7647=EDGE_CURVE ( 'NONE', #11273, #4720, #83, .T. ) ;
#7649=CARTESIAN_POINT ( 'NONE',  ( 4.999999999999999112, -1.561154383803080581, -20.18872947935932771 ) ) ;
#7659=DIRECTION ( 'NONE',  ( 0.000000000000000000, 0.000000000000000000, -1.000000000000000000 ) ) ;
#7664=VECTOR ( 'NONE', #3375, 1000.000000000000000 ) ;
#7665=CARTESIAN_POINT ( 'NONE',  ( 0.000000000000000000, 5.955107813822862362, -26.33508479058314933 ) ) ;
#7669=CIRCLE ( 'NONE', #3265, 9.600000000009604406 ) ;
#7671=DIRECTION ( 'NONE',  ( 0.000000000000000000, -0.7071067811865537900, 0.7071067811865414665 ) ) ;
#7676=ORIENTED_EDGE ( 'NONE', *, *, #10982, .F. ) ;
#7679=DIRECTION ( 'NONE',  ( 0.000000000000000000, 0.000000000000000000, -1.000000000000000000 ) ) ;
#7684=CARTESIAN_POINT ( 'NONE',  ( 4.999999999999999112, -2.791921004064401579, 22.37914155802284100 ) ) ;
#7685=CARTESIAN_POINT ( 'NONE',  ( 0.000000000000000000, -20.18872947935932061, 1.561154383803151191 ) ) ;
#7692=VERTEX_POINT ( 'NONE', #6722 ) ;
#7704=VERTEX_POINT ( 'NONE', #1833 ) ;
#7709=EDGE_CURVE ( 'NONE', #1163, #11209, #7389, .T. ) ;
#7710=EDGE_CURVE ( 'NONE', #9875, #5720, #10769, .T. ) ;
#7722=CARTESIAN_POINT ( 'NONE',  ( 4.999999999999999112, 0.000000000000000000, 0.000000000000000000 ) ) ;
#7732=ORIENTED_EDGE ( 'NONE', *, *, #8383, .F. ) ;
#7733=VERTEX_POINT ( 'NONE', #10389 ) ;
#7744=CARTESIAN_POINT ( 'NONE',  ( 4.999999999999999112, -19.60720892790245529, -11.14352537685195266 ) ) ;
#7764=AXIS2_PLACEMENT_3D ( 'NONE', #7097, #4201, #8912 ) ;
#7774=VERTEX_POINT ( 'NONE', #266 ) ;
#7782=CARTESIAN_POINT ( 'NONE',  ( 4.999999999999999112, 11.14352537685202016, -19.60720892790241265 ) ) ;
#7787=CARTESIAN_POINT ( 'NONE',  ( 5.000000000000000000, 0.000000000000000000, 0.000000000000000000 ) ) ;
#7798=VERTEX_POINT ( 'NONE', #3953 ) ;
#7803=DIRECTION ( 'NONE',  ( 0.000000000000000000, -6.866613759067995433E-15, 1.000000000000000000 ) ) ;
#7805=VERTEX_POINT ( 'NONE', #11694 ) ;
#7807=DIRECTION ( 'NONE',  ( 0.000000000000000000, 0.000000000000000000, 1.000000000000000000 ) ) ;
#7808=VERTEX_POINT ( 'NONE', #3092 ) ;
#7811=ORIENTED_EDGE ( 'NONE', *, *, #9979, .T. ) ;
#7818=DIRECTION ( 'NONE',  ( -1.000000000000000000, 0.000000000000000000, -0.000000000000000000 ) ) ;
#7851=EDGE_CURVE ( 'NONE', #9474, #11456, #9781, .T. ) ;
#7852=ORIENTED_EDGE ( 'NONE', *, *, #3332, .F. ) ;
#7856=LINE ( 'NONE', #902, #1204 ) ;
#7857=DIRECTION ( 'NONE',  ( 0.000000000000000000, 0.7071067811865439090, 0.7071067811865512365 ) ) ;
#7871=CARTESIAN_POINT ( 'NONE',  ( 0.000000000000000000, 21.74405275335758247, 5.984728032765037398 ) ) ;
#7876=CARTESIAN_POINT ( 'NONE',  ( 4.999999999999999112, -4.576198416197066798, -26.60936692326695407 ) ) ;
#7877=ORIENTED_EDGE ( 'NONE', *, *, #3877, .F. ) ;
#7886=ORIENTED_EDGE ( 'NONE', *, *, #6498, .T. ) ;
#7888=DIRECTION ( 'NONE',  ( -1.000000000000000000, 0.000000000000000000, 0.000000000000000000 ) ) ;
#7892=AXIS2_PLACEMENT_3D ( 'NONE', #11946, #1654, #10149 ) ;
#7893=DIRECTION ( 'NONE',  ( -1.000000000000000000, 0.000000000000000000, -0.000000000000000000 ) ) ;
#7898=DIRECTION ( 'NONE',  ( -1.000000000000000000, 0.000000000000000000, 0.000000000000000000 ) ) ;
#7900=FACE_OUTER_BOUND ( 'NONE', #11642, .T. ) ;
#7905=ORIENTED_EDGE ( 'NONE', *, *, #9903, .F. ) ;
#7907=AXIS2_PLACEMENT_3D ( 'NONE', #3004, #7945, #3436 ) ;
#7911=CYLINDRICAL_SURFACE ( 'NONE', #1405, 27.00000000002699707 ) ;
#7922=ADVANCED_FACE ( 'NONE', ( #11747 ), #3206, .T. ) ;
#7924=VERTEX_POINT ( 'NONE', #7020 ) ;
#7935=DIRECTION ( 'NONE',  ( 0.000000000000000000, -0.9238795325112906243, 0.3826834323650805114 ) ) ;
#7939=EDGE_LOOP ( 'NONE', ( #8437, #6746, #6086, #6619 ) ) ;
#7942=ORIENTED_EDGE ( 'NONE', *, *, #3568, .T. ) ;
#7945=DIRECTION ( 'NONE',  ( -1.000000000000000000, -0.000000000000000000, -0.000000000000000000 ) ) ;
#7953=DIRECTION ( 'NONE',  ( 1.000000000000000000, 0.000000000000000000, 0.000000000000000000 ) ) ;
#7962=DIRECTION ( 'NONE',  ( -1.000000000000000000, -0.000000000000000000, -0.000000000000000000 ) ) ;
#7964=LINE ( 'NONE', #11884, #9602 ) ;
#7967=CYLINDRICAL_SURFACE ( 'NONE', #2236, 9.600000000009600853 ) ;
#7973=ORIENTED_EDGE ( 'NONE', *, *, #5022, .T. ) ;
#7974=EDGE_CURVE ( 'NONE', #2061, #10053, #5575, .T. ) ;
#7981=DIRECTION ( 'NONE',  ( 0.000000000000000000, 0.000000000000000000, -1.000000000000000000 ) ) ;
#7982=DIRECTION ( 'NONE',  ( 1.000000000000000000, 0.000000000000000000, 0.000000000000000000 ) ) ;
#7984=CYLINDRICAL_SURFACE ( 'NONE', #5246, 20.24900000002024569 ) ;
#7994=ADVANCED_FACE ( 'NONE', ( #1928 ), #2921, .T. ) ;
#8007=ADVANCED_FACE ( 'NONE', ( #225 ), #4045, .T. ) ;
#8015=CIRCLE ( 'NONE', #9811, 9.600000000009600853 ) ;
#8018=CYLINDRICAL_SURFACE ( 'NONE', #5810, 20.24900000002024569 ) ;
#8023=DIRECTION ( 'NONE',  ( 1.000000000000000000, 0.000000000000000000, 0.000000000000000000 ) ) ;
#8027=EDGE_CURVE ( 'NONE', #7435, #7808, #8796, .T. ) ;
#8030=ORIENTED_EDGE ( 'NONE', *, *, #2971, .T. ) ;
#8039=CARTESIAN_POINT ( 'NONE',  ( 4.999999999999999112, 22.37914155802285876, -2.791921004064323864 ) ) ;
#8041=VERTEX_POINT ( 'NONE', #1105 ) ;
#8043=FACE_OUTER_BOUND ( 'NONE', #5502, .T. ) ;
#8050=ORIENTED_EDGE ( 'NONE', *, *, #2489, .T. ) ;
#8054=AXIS2_PLACEMENT_3D ( 'NONE', #11082, #703, #1830 ) ;
#8056=CIRCLE ( 'NONE', #12222, 9.600000000009600853 ) ;
#8059=PLANE ( 'NONE',  #3226 ) ;
#8075=ORIENTED_EDGE ( 'NONE', *, *, #10894, .T. ) ;
#8076=CARTESIAN_POINT ( 'NONE',  ( -10.00000000000000000, 0.000000000000000000, 0.000000000000000000 ) ) ;
#8081=VERTEX_POINT ( 'NONE', #4862 ) ;
#8082=LINE ( 'NONE', #5070, #992 ) ;
#8103=FACE_OUTER_BOUND ( 'NONE', #2263, .T. ) ;
#8108=AXIS2_PLACEMENT_3D ( 'NONE', #6124, #3943, #8895 ) ;
#8114=EDGE_CURVE ( 'NONE', #474, #3672, #6187, .T. ) ;
#8120=DIRECTION ( 'NONE',  ( -1.000000000000000000, 0.000000000000000000, 0.000000000000000000 ) ) ;
#8124=DIRECTION ( 'NONE',  ( 0.000000000000000000, 0.000000000000000000, -1.000000000000000000 ) ) ;
#8135=ADVANCED_FACE ( 'NONE', ( #1286 ), #9974, .T. ) ;
#8147=EDGE_CURVE ( 'NONE', #9896, #2664, #11370, .T. ) ;
#8150=ADVANCED_FACE ( 'NONE', ( #6228 ), #11712, .T. ) ;
#8153=CARTESIAN_POINT ( 'NONE',  ( 0.000000000000000000, 17.79862902732265084, 13.85025647830063100 ) ) ;
#8156=VERTEX_POINT ( 'NONE', #6157 ) ;
#8160=DIRECTION ( 'NONE',  ( 0.000000000000000000, 0.000000000000000000, 1.000000000000000000 ) ) ;
#8161=UNCERTAINTY_MEASURE_WITH_UNIT (LENGTH_MEASURE( 1.000000000000000082E-05 ), #425, 'distance_accuracy_value', 'NONE');
#8168=CIRCLE ( 'NONE', #4557, 9.600000000009599077 ) ;
#8171=ORIENTED_EDGE ( 'NONE', *, *, #8767, .F. ) ;
#8174=EDGE_CURVE ( 'NONE', #7438, #5310, #1477, .T. ) ;
#8177=AXIS2_PLACEMENT_3D ( 'NONE', #10917, #12041, #7314 ) ;
#8180=ORIENTED_EDGE ( 'NONE', *, *, #9866, .T. ) ;
#8185=DIRECTION ( 'NONE',  ( -1.000000000000000000, -0.000000000000000000, 0.000000000000000000 ) ) ;
#8188=VERTEX_POINT ( 'NONE', #5291 ) ;
#8189=DIRECTION ( 'NONE',  ( -1.000000000000000000, 0.000000000000000000, -0.000000000000000000 ) ) ;
#8195=DIRECTION ( 'NONE',  ( 0.000000000000000000, -0.7071067811865389130, -0.7071067811865561215 ) ) ;
#8196=CARTESIAN_POINT ( 'NONE',  ( 0.000000000000000000, 22.37914155802285876, 6.808078995945277434 ) ) ;
#8197=AXIS2_PLACEMENT_3D ( 'NONE', #8039, #11759, #11935 ) ;
#8208=VECTOR ( 'NONE', #10382, 1000.000000000000000 ) ;
#8209=AXIS2_PLACEMENT_3D ( 'NONE', #3011, #5951, #370 ) ;
#8213=EDGE_CURVE ( 'NONE', #11053, #3803, #1401, .T. ) ;
#8214=CARTESIAN_POINT ( 'NONE',  ( 4.999999999999999112, 0.000000000000000000, 0.000000000000000000 ) ) ;
#8216=EDGE_LOOP ( 'NONE', ( #5552, #9495, #2868, #5693, #1853, #2871, #3749, #9264, #6844, #9122, #4878, #5473, #8433, #747, #8971, #10731, #623, #3530, #11719, #12340, #7122, #1805, #5077, #10194, #1769, #3579, #5968, #2229, #4977, #2357, #6167, #6779, #7877, #4972, #10020, #3851, #874, #11307, #1579, #10592, #11262, #6883, #10749, #6279, #289, #8458, #7343, #1978, #4505, #1669, #4461, #10740, #357, #232, #8662, #4785, #12077, #10410, #5281, #6073, #1393, #11717, #7212, #5961, #5272, #845, #7089, #3330, #7811 ) ) ;
#8218=CARTESIAN_POINT ( 'NONE',  ( -10.00000000000000000, 0.000000000000000000, 0.000000000000000000 ) ) ;
#8221=CIRCLE ( 'NONE', #2219, 27.00000000002699707 ) ;
#8223=CYLINDRICAL_SURFACE ( 'NONE', #3894, 9.600000000009597301 ) ;
#8226=ORIENTED_EDGE ( 'NONE', *, *, #3058, .T. ) ;
#8233=DIRECTION ( 'NONE',  ( 0.000000000000000000, 0.000000000000000000, 1.000000000000000000 ) ) ;
#8237=LINE ( 'NONE', #6482, #3820 ) ;
#8238=EDGE_LOOP ( 'NONE', ( #8381, #10686, #2798, #10957 ) ) ;
#8241=CARTESIAN_POINT ( 'NONE',  ( 0.000000000000000000, -18.05452603534171985, 9.168210874537514599 ) ) ;
#8252=VERTEX_POINT ( 'NONE', #6346 ) ;
#8258=VERTEX_POINT ( 'NONE', #9236 ) ;
#8259=AXIS2_PLACEMENT_3D ( 'NONE', #8509, #6705, #2806 ) ;
#8261=ORIENTED_EDGE ( 'NONE', *, *, #7000, .T. ) ;
#8264=CARTESIAN_POINT ( 'NONE',  ( 0.000000000000000000, 15.57980286237472889, 22.05152472667135655 ) ) ;
#8271=EDGE_LOOP ( 'NONE', ( #742, #1635, #12325, #4765 ) ) ;
#8277=DIRECTION ( 'NONE',  ( 0.000000000000000000, 0.000000000000000000, -1.000000000000000000 ) ) ;
#8280=CARTESIAN_POINT ( 'NONE',  ( 2.499999999999999556, 14.41081992069310225, 22.83261415639507419 ) ) ;
#8281=CYLINDRICAL_SURFACE ( 'NONE', #8054, 9.600000000009600853 ) ;
#8290=ADVANCED_FACE ( 'NONE', ( #11276 ), #11215, .T. ) ;
#8303=EDGE_CURVE ( 'NONE', #11016, #1740, #3478, .T. ) ;
#8305=ADVANCED_FACE ( 'NONE', ( #11149 ), #10330, .T. ) ;
#8311=ORIENTED_EDGE ( 'NONE', *, *, #886, .T. ) ;
#8313=DIRECTION ( 'NONE',  ( -1.000000000000000000, -0.000000000000000000, -0.000000000000000000 ) ) ;
#8314=ORIENTED_EDGE ( 'NONE', *, *, #6887, .F. ) ;
#8321=VERTEX_POINT ( 'NONE', #10220 ) ;
#8324=CARTESIAN_POINT ( 'NONE',  ( -10.00000000000000000, 0.000000000000000000, 0.000000000000000000 ) ) ;
#8331=CARTESIAN_POINT ( 'NONE',  ( 2.499999999999999556, 22.83261415639503156, 14.41081992069317330 ) ) ;
#8335=CARTESIAN_POINT ( 'NONE',  ( 4.999999999999999112, -21.74405275335762155, 5.984728032764886407 ) ) ;
#8340=DIRECTION ( 'NONE',  ( -1.000000000000000000, 0.000000000000000000, 0.000000000000000000 ) ) ;
#8343=CARTESIAN_POINT ( 'NONE',  ( 4.999999999999999112, -21.74405275335762155, 5.984728032764886407 ) ) ;
#8344=DIRECTION ( 'NONE',  ( 0.000000000000000000, 0.000000000000000000, -1.000000000000000000 ) ) ;
#8345=CARTESIAN_POINT ( 'NONE',  ( 4.999999999999999112, -13.85025647830069317, 17.79862902732260110 ) ) ;
#8346=DIRECTION ( 'NONE',  ( 0.000000000000000000, -0.7071067811865389130, -0.7071067811865561215 ) ) ;
#8348=ORIENTED_EDGE ( 'NONE', *, *, #7107, .F. ) ;
#8351=CYLINDRICAL_SURFACE ( 'NONE', #9666, 9.600000000009600853 ) ;
#8358=CIRCLE ( 'NONE', #10944, 9.600000000009600853 ) ;
#8360=CARTESIAN_POINT ( 'NONE',  ( 4.999999999999999112, 0.000000000000000000, 0.000000000000000000 ) ) ;
#8362=ORIENTED_EDGE ( 'NONE', *, *, #5993, .T. ) ;
#8368=PRESENTATION_STYLE_ASSIGNMENT (( #2928 ) ) ;
#8370=CARTESIAN_POINT ( 'NONE',  ( 4.999999999999999112, 0.000000000000000000, 0.000000000000000000 ) ) ;
#8372=DIRECTION ( 'NONE',  ( 0.000000000000000000, -0.3826834323650773473, -0.9238795325112919565 ) ) ;
#8374=CIRCLE ( 'NONE', #1173, 9.600000000009600853 ) ;
#8381=ORIENTED_EDGE ( 'NONE', *, *, #9742, .F. ) ;
#8383=EDGE_CURVE ( 'NONE', #1305, #474, #3602, .T. ) ;
#8384=DIRECTION ( 'NONE',  ( 0.000000000000000000, 1.000000000000000000, 3.614007241614734605E-15 ) ) ;
#8387=AXIS2_PLACEMENT_3D ( 'NONE', #10515, #12192, #1900 ) ;
#8390=EDGE_LOOP ( 'NONE', ( #11551, #6644, #6489, #7276 ) ) ;
#8394=DIRECTION ( 'NONE',  ( 1.000000000000000000, -0.000000000000000000, -0.000000000000000000 ) ) ;
#8398=EDGE_CURVE ( 'NONE', #10665, #11209, #7856, .T. ) ;
#8419=EDGE_LOOP ( 'NONE', ( #9407, #10354, #11539, #624 ) ) ;
#8424=ORIENTED_EDGE ( 'NONE', *, *, #9544, .F. ) ;
#8433=ORIENTED_EDGE ( 'NONE', *, *, #12309, .T. ) ;
#8434=CARTESIAN_POINT ( 'NONE',  ( 0.000000000000000000, 0.000000000000000000, 20.24900000002024569 ) ) ;
#8437=ORIENTED_EDGE ( 'NONE', *, *, #8174, .T. ) ;
#8438=AXIS2_PLACEMENT_3D ( 'NONE', #8824, #7893, #360 ) ;
#8444=VECTOR ( 'NONE', #11886, 1000.000000000000000 ) ;
#8451=VERTEX_POINT ( 'NONE', #3774 ) ;
#8457=CIRCLE ( 'NONE', #75, 9.600000000009600853 ) ;
#8458=ORIENTED_EDGE ( 'NONE', *, *, #6933, .T. ) ;
#8461=ADVANCED_FACE ( 'NONE', ( #3960 ), #5774, .T. ) ;
#8464=( NAMED_UNIT ( * ) PLANE_ANGLE_UNIT ( ) SI_UNIT ( $, .RADIAN. ) );
#8470=VERTEX_POINT ( 'NONE', #6784 ) ;
#8472=LINE ( 'NONE', #12128, #1824 ) ;
#8473=VERTEX_POINT ( 'NONE', #10585 ) ;
#8491=ADVANCED_FACE ( 'NONE', ( #3155 ), #275, .T. ) ;
#8498=DIRECTION ( 'NONE',  ( -1.000000000000000000, 0.000000000000000000, -0.000000000000000000 ) ) ;
#8500=DIRECTION ( 'NONE',  ( -1.000000000000000000, 0.000000000000000000, 0.000000000000000000 ) ) ;
#8509=CARTESIAN_POINT ( 'NONE',  ( 0.000000000000000000, 0.000000000000000000, 0.000000000000000000 ) ) ;
#8515=CYLINDRICAL_SURFACE ( 'NONE', #5899, 20.24900000002024569 ) ;
#8516=ADVANCED_FACE ( 'NONE', ( #2205 ), #5140, .T. ) ;
#8519=CARTESIAN_POINT ( 'NONE',  ( 4.999999999999999112, 19.60720892790252989, 11.14352537685181588 ) ) ;
#8525=DIRECTION ( 'NONE',  ( 0.000000000000000000, -0.7071067811865389130, -0.7071067811865561215 ) ) ;
#8530=EDGE_CURVE ( 'NONE', #536, #11283, #7964, .T. ) ;
#8539=ORIENTED_EDGE ( 'NONE', *, *, #9635, .F. ) ;
#8540=ORIENTED_EDGE ( 'NONE', *, *, #1462, .T. ) ;
#8544=ADVANCED_FACE ( 'NONE', ( #8103 ), #7911, .T. ) ;
#8549=DIRECTION ( 'NONE',  ( -1.000000000000000000, 0.000000000000000000, -0.000000000000000000 ) ) ;
#8550=ORIENTED_EDGE ( 'NONE', *, *, #3332, .T. ) ;
#8551=ORIENTED_EDGE ( 'NONE', *, *, #3267, .F. ) ;
#8561=CARTESIAN_POINT ( 'NONE',  ( 0.000000000000000000, 15.57980286237503442, -22.05152472667113983 ) ) ;
#8562=EDGE_LOOP ( 'NONE', ( #308, #2727, #9525, #2622 ) ) ;
#8564=VECTOR ( 'NONE', #4141, 1000.000000000000000 ) ;
#8565=DIRECTION ( 'NONE',  ( 0.000000000000000000, 0.3826834323650841196, 0.9238795325112890700 ) ) ;
#8566=CIRCLE ( 'NONE', #5569, 9.600000000009600853 ) ;
#8567=CARTESIAN_POINT ( 'NONE',  ( 2.499999999999999556, -15.57980286237457435, -22.05152472667146668 ) ) ;
#8571=CARTESIAN_POINT ( 'NONE',  ( 4.999999999999999112, -18.05452603534171985, 9.168210874537514599 ) ) ;
#8578=AXIS2_PLACEMENT_3D ( 'NONE', #9500, #923, #5804 ) ;
#8579=CYLINDRICAL_SURFACE ( 'NONE', #7011, 27.00000000002699707 ) ;
#8582=DIRECTION ( 'NONE',  ( 1.000000000000000000, -0.000000000000000000, 0.000000000000000000 ) ) ;
#8593=CARTESIAN_POINT ( 'NONE',  ( 4.999999999999999112, 0.000000000000000000, 0.000000000000000000 ) ) ;
#8595=EDGE_CURVE ( 'NONE', #4367, #2664, #5332, .T. ) ;
#8598=ORIENTED_EDGE ( 'NONE', *, *, #3489, .T. ) ;
#8612=EDGE_CURVE ( 'NONE', #978, #7155, #10091, .T. ) ;
#8618=EDGE_CURVE ( 'NONE', #8041, #8258, #11198, .T. ) ;
#8619=EDGE_LOOP ( 'NONE', ( #9559, #7006, #5769, #10464 ) ) ;
#8621=EDGE_LOOP ( 'NONE', ( #2902, #4377, #2162, #6733 ) ) ;
#8630=VECTOR ( 'NONE', #12040, 1000.000000000000000 ) ;
#8634=AXIS2_PLACEMENT_3D ( 'NONE', #10255, #626, #1751 ) ;
#8646=VECTOR ( 'NONE', #8120, 1000.000000000000000 ) ;
#8647=EDGE_CURVE ( 'NONE', #1819, #11306, #4571, .T. ) ;
#8648=AXIS2_PLACEMENT_3D ( 'NONE', #12299, #3692, #10308 ) ;
#8655=DIRECTION ( 'NONE',  ( -1.000000000000000000, 0.000000000000000000, 0.000000000000000000 ) ) ;
#8659=CARTESIAN_POINT ( 'NONE',  ( 50.00005079999999680, 0.000000000000000000, 0.000000000000000000 ) ) ;
#8661=MANIFOLD_SOLID_BREP ( 'Keyway', #177 ) ;
#8662=ORIENTED_EDGE ( 'NONE', *, *, #2118, .T. ) ;
#8668=VERTEX_POINT ( 'NONE', #3520 ) ;
#8677=EDGE_CURVE ( 'NONE', #6998, #9896, #11499, .T. ) ;
#8683=DIRECTION ( 'NONE',  ( -1.000000000000000000, -0.000000000000000000, -0.000000000000000000 ) ) ;
#8693=VERTEX_POINT ( 'NONE', #12307 ) ;
#8695=EDGE_CURVE ( 'NONE', #4331, #5656, #8015, .T. ) ;
#8699=DIRECTION ( 'NONE',  ( -1.000000000000000000, 0.000000000000000000, -0.000000000000000000 ) ) ;
#8711=DIRECTION ( 'NONE',  ( 1.000000000000000000, 0.000000000000000000, 0.000000000000000000 ) ) ;
#8734=DIRECTION ( 'NONE',  ( 0.000000000000000000, 0.000000000000000000, 1.000000000000000000 ) ) ;
#8740=CARTESIAN_POINT ( 'NONE',  ( 4.999999999999999112, 0.000000000000000000, 0.000000000000000000 ) ) ;
#8745=ORIENTED_EDGE ( 'NONE', *, *, #8618, .T. ) ;
#8746=CARTESIAN_POINT ( 'NONE',  ( 4.999999999999999112, 21.74405275335758247, 5.984728032765037398 ) ) ;
#8749=ADVANCED_FACE ( 'NONE', ( #5703 ), #8579, .T. ) ;
#8752=DIRECTION ( 'NONE',  ( 1.000000000000000000, 0.000000000000000000, -0.000000000000000000 ) ) ;
#8755=ORIENTED_EDGE ( 'NONE', *, *, #3142, .T. ) ;
#8762=VECTOR ( 'NONE', #8752, 1000.000000000000000 ) ;
#8766=ADVANCED_FACE ( 'NONE', ( #6839 ), #3830, .T. ) ;
#8767=EDGE_CURVE ( 'NONE', #2800, #11007, #2751, .T. ) ;
#8771=ORIENTED_EDGE ( 'NONE', *, *, #12313, .T. ) ;
#8772=CARTESIAN_POINT ( 'NONE',  ( 4.999999999999999112, 0.000000000000000000, 0.000000000000000000 ) ) ;
#8773=CARTESIAN_POINT ( 'NONE',  ( 4.999999999999999112, 22.83261415639502800, 14.41081992069317330 ) ) ;
#8774=VECTOR ( 'NONE', #854, 1000.000000000000000 ) ;
#8777=AXIS2_PLACEMENT_3D ( 'NONE', #4352, #8185, #3430 ) ;
#8783=EDGE_CURVE ( 'NONE', #4084, #5720, #1259, .T. ) ;
#8788=CIRCLE ( 'NONE', #4982, 9.600000000009604406 ) ;
#8791=EDGE_LOOP ( 'NONE', ( #12140, #7255, #1902, #6197 ) ) ;
#8796=CIRCLE ( 'NONE', #1668, 27.00000000002699707 ) ;
#8802=DIRECTION ( 'NONE',  ( 0.000000000000000000, 0.000000000000000000, 1.000000000000000000 ) ) ;
#8810=CARTESIAN_POINT ( 'NONE',  ( 2.499999999999999556, -4.576198416197066798, -26.60936692326695407 ) ) ;
#8817=AXIS2_PLACEMENT_3D ( 'NONE', #9486, #719, #4532 ) ;
#8824=CARTESIAN_POINT ( 'NONE',  ( 4.999999999999999112, 13.85025647830082818, -17.79862902732250163 ) ) ;
#8837=DIRECTION ( 'NONE',  ( -1.000000000000000000, -0.000000000000000000, 0.000000000000000000 ) ) ;
#8839=LINE ( 'NONE', #4947, #6447 ) ;
#8840=EDGE_LOOP ( 'NONE', ( #2970, #6995, #151, #3052 ) ) ;
#8850=ORIENTED_EDGE ( 'NONE', *, *, #174, .F. ) ;
#8852=EDGE_CURVE ( 'NONE', #1528, #6266, #5209, .T. ) ;
#8863=EDGE_LOOP ( 'NONE', ( #918, #12111, #5939, #9736 ) ) ;
#8864=DIRECTION ( 'NONE',  ( 1.000000000000000000, 0.000000000000000000, 0.000000000000000000 ) ) ;
#8868=ADVANCED_BREP_SHAPE_REPRESENTATION ( '', ( #8661, #6056 ), #3048 ) ;
#8869=ORIENTED_EDGE ( 'NONE', *, *, #9979, .F. ) ;
#8871=AXIS2_PLACEMENT_3D ( 'NONE', #11005, #2371, #6324 ) ;
#8876=FACE_OUTER_BOUND ( 'NONE', #8621, .T. ) ;
#8877=DIRECTION ( 'NONE',  ( 0.000000000000000000, 0.000000000000000000, 1.000000000000000000 ) ) ;
#8879=ORIENTED_EDGE ( 'NONE', *, *, #343, .T. ) ;
#8880=VECTOR ( 'NONE', #2745, 1000.000000000000000 ) ;
#8888=CARTESIAN_POINT ( 'NONE',  ( 4.999999999999999112, 22.37914155802285876, -2.791921004064323864 ) ) ;
#8892=ORIENTED_EDGE ( 'NONE', *, *, #1420, .T. ) ;
#8893=CIRCLE ( 'NONE', #3492, 20.24900000002024925 ) ;
#8895=DIRECTION ( 'NONE',  ( 0.000000000000000000, 0.000000000000000000, 1.000000000000000000 ) ) ;
#8897=DIRECTION ( 'NONE',  ( 0.000000000000000000, 0.000000000000000000, 1.000000000000000000 ) ) ;
#8900=DIRECTION ( 'NONE',  ( -1.000000000000000000, -0.000000000000000000, 0.000000000000000000 ) ) ;
#8911=DIRECTION ( 'NONE',  ( 0.000000000000000000, -0.7071067811865537900, 0.7071067811865414665 ) ) ;
#8912=DIRECTION ( 'NONE',  ( 0.000000000000000000, 0.000000000000000000, 1.000000000000000000 ) ) ;
#8915=DIRECTION ( 'NONE',  ( -1.000000000000000000, 0.000000000000000000, 0.000000000000000000 ) ) ;
#8924=CARTESIAN_POINT ( 'NONE',  ( 4.999999999999999112, -17.79862902732255137, -13.85025647830076245 ) ) ;
#8927=CARTESIAN_POINT ( 'NONE',  ( 0.000000000000000000, -21.74405275335762155, 5.984728032764886407 ) ) ;
#8936=CARTESIAN_POINT ( 'NONE',  ( 4.999999999999999112, 2.791921004064568113, -22.37914155802282323 ) ) ;
#8942=CARTESIAN_POINT ( 'NONE',  ( 2.499999999999999556, -14.41081992069326034, 22.83261415639497471 ) ) ;
#8959=ORIENTED_EDGE ( 'NONE', *, *, #3540, .F. ) ;
#8965=CARTESIAN_POINT ( 'NONE',  ( 4.999999999999999112, -22.37914155802283034, -2.791921004064479739 ) ) ;
#8971=ORIENTED_EDGE ( 'NONE', *, *, #189, .T. ) ;
#8976=EDGE_CURVE ( 'NONE', #7774, #4444, #4822, .T. ) ;
#8980=FACE_OUTER_BOUND ( 'NONE', #9156, .T. ) ;
#8985=DIRECTION ( 'NONE',  ( -1.000000000000000000, -0.000000000000000000, 0.000000000000000000 ) ) ;
#8991=VERTEX_POINT ( 'NONE', #12287 ) ;
#8993=DIRECTION ( 'NONE',  ( 1.000000000000000000, -0.000000000000000000, 0.000000000000000000 ) ) ;
#8994=EDGE_CURVE ( 'NONE', #3875, #5016, #1733, .T. ) ;
#8999=VECTOR ( 'NONE', #2469, 1000.000000000000000 ) ;
#9008=CYLINDRICAL_SURFACE ( 'NONE', #7907, 27.00000000002699707 ) ;
#9011=ORIENTED_EDGE ( 'NONE', *, *, #979, .F. ) ;
#9021=DIRECTION ( 'NONE',  ( 0.000000000000000000, 0.000000000000000000, -1.000000000000000000 ) ) ;
#9032=DIRECTION ( 'NONE',  ( -1.000000000000000000, 0.000000000000000000, 0.000000000000000000 ) ) ;
#9033=EDGE_CURVE ( 'NONE', #10418, #4328, #10996, .T. ) ;
#9041=CARTESIAN_POINT ( 'NONE',  ( 4.999999999999999112, -11.14352537685160982, -19.60720892790264713 ) ) ;
#9053=CIRCLE ( 'NONE', #10425, 20.24900000002024569 ) ;
#9072=DIRECTION ( 'NONE',  ( 0.000000000000000000, 0.000000000000000000, 1.000000000000000000 ) ) ;
#9078=ADVANCED_FACE ( 'NONE', ( #3169 ), #9740, .F. ) ;
#9083=DIRECTION ( 'NONE',  ( -1.000000000000000000, 0.000000000000000000, -0.000000000000000000 ) ) ;
#9084=DIRECTION ( 'NONE',  ( 0.000000000000000000, -0.3826834323650971648, 0.9238795325112837409 ) ) ;
#9085=DIRECTION ( 'NONE',  ( -1.000000000000000000, -0.000000000000000000, -0.000000000000000000 ) ) ;
#9096=ORIENTED_EDGE ( 'NONE', *, *, #6557, .T. ) ;
#9105=CYLINDRICAL_SURFACE ( 'NONE', #11619, 9.600000000009600853 ) ;
#9109=CARTESIAN_POINT ( 'NONE',  ( 4.999999999999999112, -15.57980286237488343, 22.05152472667124286 ) ) ;
#9119=FACE_OUTER_BOUND ( 'NONE', #7544, .T. ) ;
#9122=ORIENTED_EDGE ( 'NONE', *, *, #7709, .T. ) ;
#9126=LINE ( 'NONE', #5169, #11574 ) ;
#9130=CYLINDRICAL_SURFACE ( 'NONE', #304, 27.00000000002699707 ) ;
#9132=DIRECTION ( 'NONE',  ( -1.000000000000000000, 0.000000000000000000, 0.000000000000000000 ) ) ;
#9139=DIRECTION ( 'NONE',  ( -1.000000000000000000, 0.000000000000000000, 0.000000000000000000 ) ) ;
#9141=ORIENTED_EDGE ( 'NONE', *, *, #645, .F. ) ;
#9149=EDGE_CURVE ( 'NONE', #1032, #8188, #5827, .T. ) ;
#9153=CARTESIAN_POINT ( 'NONE',  ( 4.999999999999999112, 15.37949036966230132, -13.17168466712912434 ) ) ;
#9154=LINE ( 'NONE', #10846, #6444 ) ;
#9155=DIRECTION ( 'NONE',  ( 0.000000000000000000, 0.000000000000000000, 1.000000000000000000 ) ) ;
#9156=EDGE_LOOP ( 'NONE', ( #5361, #690, #6795, #2369 ) ) ;
#9163=EDGE_CURVE ( 'NONE', #11283, #8451, #6427, .T. ) ;
#9170=DIRECTION ( 'NONE',  ( 0.000000000000000000, 0.000000000000000000, -1.000000000000000000 ) ) ;
#9176=ORIENTED_EDGE ( 'NONE', *, *, #12309, .F. ) ;
#9182=ORIENTED_EDGE ( 'NONE', *, *, #9856, .T. ) ;
#9183=CARTESIAN_POINT ( 'NONE',  ( 4.999999999999999112, 19.24938187143296275, 6.283573709965379450 ) ) ;
#9185=AXIS2_PLACEMENT_3D ( 'NONE', #1687, #9083, #7192 ) ;
#9190=CARTESIAN_POINT ( 'NONE',  ( -10.00000000000000000, 0.000000000000000000, 0.000000000000000000 ) ) ;
#9193=AXIS2_PLACEMENT_3D ( 'NONE', #8924, #7164, #338 ) ;
#9196=DIRECTION ( 'NONE',  ( 0.000000000000000000, 0.000000000000000000, 1.000000000000000000 ) ) ;
#9198=DIRECTION ( 'NONE',  ( 0.000000000000000000, 0.000000000000000000, 1.000000000000000000 ) ) ;
#9199=ORIENTED_EDGE ( 'NONE', *, *, #6247, .F. ) ;
#9200=ORIENTED_EDGE ( 'NONE', *, *, #10574, .F. ) ;
#9201=EDGE_CURVE ( 'NONE', #2664, #238, #8221, .T. ) ;
#9208=CYLINDRICAL_SURFACE ( 'NONE', #5092, 9.600000000009600853 ) ;
#9209=EDGE_CURVE ( 'NONE', #11506, #2800, #1031, .T. ) ;
#9211=LINE ( 'NONE', #6461, #4036 ) ;
#9212=( GEOMETRIC_REPRESENTATION_CONTEXT ( 3 ) GLOBAL_UNCERTAINTY_ASSIGNED_CONTEXT ( ( #6776 ) ) GLOBAL_UNIT_ASSIGNED_CONTEXT ( ( #636, #8464, #2455 ) ) REPRESENTATION_CONTEXT ( 'NONE', 'WORKASPACE' ) );
#9217=DIRECTION ( 'NONE',  ( 0.000000000000000000, 0.3826834323650905589, -0.9238795325112864054 ) ) ;
#9218=CARTESIAN_POINT ( 'NONE',  ( 4.999999999999999112, 2.791921004064247480, 22.37914155802286942 ) ) ;
#9222=CARTESIAN_POINT ( 'NONE',  ( 0.000000000000000000, -1.561154383803080581, -20.18872947935932771 ) ) ;
#9223=AXIS2_PLACEMENT_3D ( 'NONE', #1229, #6927, #10728 ) ;
#9230=VERTEX_POINT ( 'NONE', #11039 ) ;
#9231=VECTOR ( 'NONE', #411, 1000.000000000000000 ) ;
#9236=CARTESIAN_POINT ( 'NONE',  ( 0.000000000000000000, -9.168210874537445321, -18.05452603534175893 ) ) ;
#9241=DIRECTION ( 'NONE',  ( 0.000000000000000000, 0.000000000000000000, 1.000000000000000000 ) ) ;
#9245=FACE_OUTER_BOUND ( 'NONE', #11471, .T. ) ;
#9249=ADVANCED_FACE ( 'NONE', ( #12030, #2471 ), #7301, .F. ) ;
#9258=EDGE_CURVE ( 'NONE', #7733, #11506, #5294, .T. ) ;
#9263=DIRECTION ( 'NONE',  ( 0.000000000000000000, -0.9238795325112906243, 0.3826834323650805114 ) ) ;
#9264=ORIENTED_EDGE ( 'NONE', *, *, #11271, .T. ) ;
#9265=CARTESIAN_POINT ( 'NONE',  ( 4.999999999999999112, 17.79862902732283914, -13.85025647830039119 ) ) ;
#9271=ORIENTED_EDGE ( 'NONE', *, *, #78, .F. ) ;
#9284=DIRECTION ( 'NONE',  ( -1.000000000000000000, 0.000000000000000000, -0.000000000000000000 ) ) ;
#9289=ORIENTED_EDGE ( 'NONE', *, *, #9856, .F. ) ;
#9291=CIRCLE ( 'NONE', #5684, 20.24900000002024569 ) ;
#9296=DIRECTION ( 'NONE',  ( 0.000000000000000000, 0.000000000000000000, 1.000000000000000000 ) ) ;
#9302=ORIENTED_EDGE ( 'NONE', *, *, #12172, .F. ) ;
#9304=EDGE_LOOP ( 'NONE', ( #10967, #4133, #5499, #1915 ) ) ;
#9309=VECTOR ( 'NONE', #4802, 1000.000000000000000 ) ;
#9316=ORIENTED_EDGE ( 'NONE', *, *, #8114, .F. ) ;
#9319=DIRECTION ( 'NONE',  ( -1.000000000000000000, 0.000000000000000000, 0.000000000000000000 ) ) ;
#9320=EDGE_LOOP ( 'NONE', ( #144, #9200, #8030, #8050 ) ) ;
#9321=CYLINDRICAL_SURFACE ( 'NONE', #2562, 9.600000000009600853 ) ;
#9322=EDGE_CURVE ( 'NONE', #7798, #2779, #10413, .T. ) ;
#9324=CARTESIAN_POINT ( 'NONE',  ( 4.999999999999999112, 0.000000000000000000, 0.000000000000000000 ) ) ;
#9328=ORIENTED_EDGE ( 'NONE', *, *, #10083, .T. ) ;
#9333=DIRECTION ( 'NONE',  ( 1.000000000000000000, 0.000000000000000000, -0.000000000000000000 ) ) ;
#9337=VERTEX_POINT ( 'NONE', #4221 ) ;
#9338=FACE_OUTER_BOUND ( 'NONE', #850, .T. ) ;
#9339=DIRECTION ( 'NONE',  ( 0.000000000000000000, 0.7071067811865439090, 0.7071067811865511255 ) ) ;
#9352=ORIENTED_EDGE ( 'NONE', *, *, #8677, .T. ) ;
#9367=AXIS2_PLACEMENT_3D ( 'NONE', #5727, #8549, #7494 ) ;
#9368=ORIENTED_EDGE ( 'NONE', *, *, #7157, .F. ) ;
#9376=EDGE_CURVE ( 'NONE', #7805, #6322, #10332, .T. ) ;
#9386=EDGE_CURVE ( 'NONE', #8321, #4719, #11412, .T. ) ;
#9387=LINE ( 'NONE', #5562, #6639 ) ;
#9399=ORIENTED_EDGE ( 'NONE', *, *, #5022, .F. ) ;
#9400=CARTESIAN_POINT ( 'NONE',  ( 0.000000000000000000, -22.83261415639512748, 14.41081992069302053 ) ) ;
#9407=ORIENTED_EDGE ( 'NONE', *, *, #8213, .T. ) ;
#9413=AXIS2_PLACEMENT_3D ( 'NONE', #7526, #11320, #6723 ) ;
#9416=AXIS2_PLACEMENT_3D ( 'NONE', #3301, #4284, #7169 ) ;
#9417=DIRECTION ( 'NONE',  ( -1.000000000000000000, -0.000000000000000000, -0.000000000000000000 ) ) ;
#9420=DIRECTION ( 'NONE',  ( -1.000000000000000000, 0.000000000000000000, 0.000000000000000000 ) ) ;
#9424=CARTESIAN_POINT ( 'NONE',  ( 4.999999999999999112, 0.000000000000000000, 0.000000000000000000 ) ) ;
#9427=AXIS2_PLACEMENT_3D ( 'NONE', #7415, #769, #11218 ) ;
#9440=( NAMED_UNIT ( * ) SI_UNIT ( $, .STERADIAN. ) SOLID_ANGLE_UNIT ( ) );
#9448=DIRECTION ( 'NONE',  ( -1.000000000000000000, -0.000000000000000000, 0.000000000000000000 ) ) ;
#9449=EDGE_CURVE ( 'NONE', #7924, #4331, #10158, .T. ) ;
#9459=DIRECTION ( 'NONE',  ( -1.000000000000000000, -0.000000000000000000, -0.000000000000000000 ) ) ;
#9463=CARTESIAN_POINT ( 'NONE',  ( 4.999999999999999112, 15.37949036966230132, -13.17168466712912434 ) ) ;
#9467=ORIENTED_EDGE ( 'NONE', *, *, #2698, .T. ) ;
#9470=EDGE_CURVE ( 'NONE', #11850, #7774, #6038, .T. ) ;
#9474=VERTEX_POINT ( 'NONE', #3597 ) ;
#9475=DIRECTION ( 'NONE',  ( -1.000000000000000000, 0.000000000000000000, 0.000000000000000000 ) ) ;
#9483=DIRECTION ( 'NONE',  ( -1.000000000000000000, 0.000000000000000000, -0.000000000000000000 ) ) ;
#9486=CARTESIAN_POINT ( 'NONE',  ( 0.000000000000000000, 0.000000000000000000, 0.000000000000000000 ) ) ;
#9488=DIRECTION ( 'NONE',  ( 0.000000000000000000, 0.000000000000000000, 1.000000000000000000 ) ) ;
#9489=SHAPE_DEFINITION_REPRESENTATION ( #5829, #10563 ) ;
#9495=ORIENTED_EDGE ( 'NONE', *, *, #6033, .T. ) ;
#9500=CARTESIAN_POINT ( 'NONE',  ( 4.999999999999999112, 0.000000000000000000, 0.000000000000000000 ) ) ;
#9516=ORIENTED_EDGE ( 'NONE', *, *, #3005, .F. ) ;
#9519=DIRECTION ( 'NONE',  ( -1.000000000000000000, -0.000000000000000000, -0.000000000000000000 ) ) ;
#9525=ORIENTED_EDGE ( 'NONE', *, *, #10193, .T. ) ;
#9526=DIRECTION ( 'NONE',  ( 0.000000000000000000, 0.3826834323650840641, 0.9238795325112890700 ) ) ;
#9531=EDGE_CURVE ( 'NONE', #8473, #11449, #4847, .T. ) ;
#9535=CARTESIAN_POINT ( 'NONE',  ( 0.000000000000000000, 0.000000000000000000, 0.000000000000000000 ) ) ;
#9541=DIRECTION ( 'NONE',  ( 0.000000000000000000, 0.000000000000000000, -1.000000000000000000 ) ) ;
#9544=EDGE_CURVE ( 'NONE', #8252, #11850, #10663, .T. ) ;
#9546=DIRECTION ( 'NONE',  ( 0.000000000000000000, 0.000000000000000000, 1.000000000000000000 ) ) ;
#9549=CARTESIAN_POINT ( 'NONE',  ( 4.999999999999999112, 0.000000000000000000, 0.000000000000000000 ) ) ;
#9554=CARTESIAN_POINT ( 'NONE',  ( 0.000000000000000000, 14.41081992069310047, 22.83261415639507774 ) ) ;
#9559=ORIENTED_EDGE ( 'NONE', *, *, #1732, .T. ) ;
#9561=VECTOR ( 'NONE', #5715, 1000.000000000000000 ) ;
#9571=ORIENTED_EDGE ( 'NONE', *, *, #1326, .F. ) ;
#9578=EDGE_CURVE ( 'NONE', #3907, #102, #12204, .T. ) ;
#9580=CARTESIAN_POINT ( 'NONE',  ( 0.000000000000000000, 22.37914155802281257, 2.791921004064645384 ) ) ;
#9583=ORIENTED_EDGE ( 'NONE', *, *, #4539, .F. ) ;
#9585=DIRECTION ( 'NONE',  ( -1.000000000000000000, -0.000000000000000000, 0.000000000000000000 ) ) ;
#9596=DIRECTION ( 'NONE',  ( 1.000000000000000000, 0.000000000000000000, 0.000000000000000000 ) ) ;
#9597=DIRECTION ( 'NONE',  ( 0.000000000000000000, 0.7071067811865439090, 0.7071067811865512365 ) ) ;
#9598=VERTEX_POINT ( 'NONE', #5914 ) ;
#9599=ORIENTED_EDGE ( 'NONE', *, *, #10676, .T. ) ;
#9602=VECTOR ( 'NONE', #1385, 1000.000000000000000 ) ;
#9613=DIRECTION ( 'NONE',  ( -1.000000000000000000, -0.000000000000000000, -0.000000000000000000 ) ) ;
#9616=CIRCLE ( 'NONE', #4212, 27.00000000002699707 ) ;
#9631=ORIENTED_EDGE ( 'NONE', *, *, #6813, .F. ) ;
#9635=EDGE_CURVE ( 'NONE', #12046, #2589, #3431, .T. ) ;
#9637=COLOUR_RGB ( '',1.000000000000000000, 0.9490196078431372140, 0.9098039215686274384 ) ;
#9638=AXIS2_PLACEMENT_3D ( 'NONE', #9535, #10525, #5778 ) ;
#9639=AXIS2_PLACEMENT_3D ( 'NONE', #806, #5382, #8384 ) ;
#9640=AXIS2_PLACEMENT_3D ( 'NONE', #12071, #6467, #1705 ) ;
#9641=FACE_OUTER_BOUND ( 'NONE', #10095, .T. ) ;
#9647=ORIENTED_EDGE ( 'NONE', *, *, #3294, .T. ) ;
#9648=DIRECTION ( 'NONE',  ( -1.000000000000000000, 0.000000000000000000, -0.000000000000000000 ) ) ;
#9656=AXIS2_PLACEMENT_3D ( 'NONE', #4131, #6018, #7198 ) ;
#9659=AXIS2_PLACEMENT_3D ( 'NONE', #5117, #2998, #1123 ) ;
#9665=EDGE_CURVE ( 'NONE', #5671, #3057, #11012, .T. ) ;
#9666=AXIS2_PLACEMENT_3D ( 'NONE', #10288, #848, #5596 ) ;
#9674=ORIENTED_EDGE ( 'NONE', *, *, #11112, .F. ) ;
#9679=EDGE_CURVE ( 'NONE', #7733, #9337, #12003, .T. ) ;
#9687=CYLINDRICAL_SURFACE ( 'NONE', #815, 9.600000000009600853 ) ;
#9698=EDGE_CURVE ( 'NONE', #11007, #8473, #9154, .T. ) ;
#9701=CIRCLE ( 'NONE', #2909, 20.24900000002024925 ) ;
#9710=VERTEX_POINT ( 'NONE', #2276 ) ;
#9713=DIRECTION ( 'NONE',  ( -1.000000000000000000, -0.000000000000000000, -0.000000000000000000 ) ) ;
#9714=CARTESIAN_POINT ( 'NONE',  ( 4.999999999999999112, -19.24938187143300539, 6.283573709965241783 ) ) ;
#9717=ORIENTED_EDGE ( 'NONE', *, *, #7974, .F. ) ;
#9722=EDGE_CURVE ( 'NONE', #6501, #2328, #11820, .T. ) ;
#9729=ORIENTED_EDGE ( 'NONE', *, *, #9866, .F. ) ;
#9731=ORIENTED_EDGE ( 'NONE', *, *, #3142, .F. ) ;
#9733=LINE ( 'NONE', #1976, #7284 ) ;
#9736=ORIENTED_EDGE ( 'NONE', *, *, #9722, .T. ) ;
#9737=ORIENTED_EDGE ( 'NONE', *, *, #8147, .F. ) ;
#9740=CYLINDRICAL_SURFACE ( 'NONE', #10402, 5.000000000000000000 ) ;
#9742=EDGE_CURVE ( 'NONE', #11003, #8470, #4271, .T. ) ;
#9743=ORIENTED_EDGE ( 'NONE', *, *, #4474, .T. ) ;
#9747=DIRECTION ( 'NONE',  ( -1.000000000000000000, 0.000000000000000000, 0.000000000000000000 ) ) ;
#9753=FACE_OUTER_BOUND ( 'NONE', #9874, .T. ) ;
#9755=ORIENTED_EDGE ( 'NONE', *, *, #7709, .F. ) ;
#9760=ADVANCED_FACE ( 'NONE', ( #8043 ), #10947, .T. ) ;
#9761=EDGE_CURVE ( 'NONE', #11750, #8156, #11032, .T. ) ;
#9769=CARTESIAN_POINT ( 'NONE',  ( 4.999999999999999112, -21.74405275335753984, -5.984728032765188388 ) ) ;
#9770=DIRECTION ( 'NONE',  ( -1.000000000000000000, 0.000000000000000000, 0.000000000000000000 ) ) ;
#9773=CARTESIAN_POINT ( 'NONE',  ( 4.999999999999999112, -22.37914155802283034, 6.808078995945121115 ) ) ;
#9774=PRODUCT_DEFINITION ( 'UNKNOWN', '', #1643, #2377 ) ;
#9776=ORIENTED_EDGE ( 'NONE', *, *, #3296, .T. ) ;
#9780=CARTESIAN_POINT ( 'NONE',  ( 4.999999999999999112, 17.79862902732265084, 13.85025647830063100 ) ) ;
#9781=CIRCLE ( 'NONE', #1376, 20.24900000002024569 ) ;
#9786=EDGE_CURVE ( 'NONE', #3803, #6352, #1646, .T. ) ;
#9808=CARTESIAN_POINT ( 'NONE',  ( 4.999999999999999112, -1.561154383803364798, 20.18872947935930640 ) ) ;
#9810=DIRECTION ( 'NONE',  ( 0.000000000000000000, -6.982962677686267499E-15, 1.000000000000000000 ) ) ;
#9811=AXIS2_PLACEMENT_3D ( 'NONE', #8519, #1827, #11445 ) ;
#9814=CARTESIAN_POINT ( 'NONE',  ( 50.00005079999999680, 6.799999999999999822, -1.500000000000000000 ) ) ;
#9815=ADVANCED_FACE ( 'NONE', ( #9338 ), #8281, .T. ) ;
#9818=DIRECTION ( 'NONE',  ( -1.000000000000000000, -0.000000000000000000, -0.000000000000000000 ) ) ;
#9819=DIRECTION ( 'NONE',  ( 0.000000000000000000, 0.000000000000000000, -1.000000000000000000 ) ) ;
#9825=CIRCLE ( 'NONE', #30, 9.600000000009600853 ) ;
#9836=CIRCLE ( 'NONE', #6837, 9.600000000009599077 ) ;
#9840=CARTESIAN_POINT ( 'NONE',  ( 4.999999999999999112, 21.74405275335758247, 15.58472803277463825 ) ) ;
#9850=VECTOR ( 'NONE', #10032, 1000.000000000000000 ) ;
#9851=ORIENTED_EDGE ( 'NONE', *, *, #12024, .T. ) ;
#9853=EDGE_CURVE ( 'NONE', #4492, #7733, #6652, .T. ) ;
#9855=CIRCLE ( 'NONE', #457, 5.000000000000000000 ) ;
#9856=EDGE_CURVE ( 'NONE', #4719, #6551, #11630, .T. ) ;
#9860=CARTESIAN_POINT ( 'NONE',  ( 2.499999999999999556, 4.576198416197250651, 26.60936692326691855 ) ) ;
#9862=VERTEX_POINT ( 'NONE', #12255 ) ;
#9864=CARTESIAN_POINT ( 'NONE',  ( 0.000000000000000000, 6.283573709965571297, -19.24938187143289881 ) ) ;
#9866=EDGE_CURVE ( 'NONE', #6238, #8693, #5848, .T. ) ;
#9868=EDGE_CURVE ( 'NONE', #3875, #6501, #9053, .T. ) ;
#9869=CARTESIAN_POINT ( 'NONE',  ( 0.000000000000000000, 22.37914155802285876, -2.791921004064323864 ) ) ;
#9870=CARTESIAN_POINT ( 'NONE',  ( 4.999999999999999112, -21.74405275335753984, -5.984728032765188388 ) ) ;
#9874=EDGE_LOOP ( 'NONE', ( #2543, #40, #5497, #3652 ) ) ;
#9875=VERTEX_POINT ( 'NONE', #3581 ) ;
#9878=CYLINDRICAL_SURFACE ( 'NONE', #5165, 20.24900000002024569 ) ;
#9881=ORIENTED_EDGE ( 'NONE', *, *, #10876, .T. ) ;
#9883=CARTESIAN_POINT ( 'NONE',  ( 4.999999999999999112, 1.561154383803505796, -20.18872947935929574 ) ) ;
#9896=VERTEX_POINT ( 'NONE', #6337 ) ;
#9899=CARTESIAN_POINT ( 'NONE',  ( 0.000000000000000000, -13.17168466712939257, 15.37949036966207039 ) ) ;
#9903=EDGE_CURVE ( 'NONE', #8693, #6875, #3650, .T. ) ;
#9906=CARTESIAN_POINT ( 'NONE',  ( 0.000000000000000000, -5.955107813822691831, 26.33508479058318485 ) ) ;
#9907=DIRECTION ( 'NONE',  ( 0.000000000000000000, 0.000000000000000000, 1.000000000000000000 ) ) ;
#9908=CARTESIAN_POINT ( 'NONE',  ( 2.499999999999999556, -5.955107813822691831, 26.33508479058318485 ) ) ;
#9910=DIRECTION ( 'NONE',  ( -1.000000000000000000, 0.000000000000000000, -0.000000000000000000 ) ) ;
#9912=ADVANCED_FACE ( 'NONE', ( #12070 ), #5465, .T. ) ;
#9914=ORIENTED_EDGE ( 'NONE', *, *, #2100, .T. ) ;
#9918=ORIENTED_EDGE ( 'NONE', *, *, #9665, .F. ) ;
#9927=CARTESIAN_POINT ( 'NONE',  ( 4.999999999999999112, 21.74405275335758247, 15.58472803277463825 ) ) ;
#9930=ORIENTED_EDGE ( 'NONE', *, *, #10243, .T. ) ;
#9931=CARTESIAN_POINT ( 'NONE',  ( 4.999999999999999112, 6.283573709965309284, 19.24938187143298052 ) ) ;
#9933=DIRECTION ( 'NONE',  ( 0.000000000000000000, 0.000000000000000000, 1.000000000000000000 ) ) ;
#9947=DIRECTION ( 'NONE',  ( 0.000000000000000000, 0.9238795325112851842, 0.3826834323650938896 ) ) ;
#9959=FACE_OUTER_BOUND ( 'NONE', #8238, .T. ) ;
#9960=EDGE_CURVE ( 'NONE', #11122, #5671, #1055, .T. ) ;
#9964=VERTEX_POINT ( 'NONE', #4758 ) ;
#9965=CARTESIAN_POINT ( 'NONE',  ( 4.999999999999997335, 6.799999999999999822, -1.500000000000000000 ) ) ;
#9972=CARTESIAN_POINT ( 'NONE',  ( 4.999999999999999112, -15.37949036966202598, -13.17168466712944408 ) ) ;
#9974=CYLINDRICAL_SURFACE ( 'NONE', #1595, 9.600000000009600853 ) ;
#9979=EDGE_CURVE ( 'NONE', #997, #7460, #2447, .T. ) ;
#9991=AXIS2_PLACEMENT_3D ( 'NONE', #10103, #11772, #7110 ) ;
#10003=ORIENTED_EDGE ( 'NONE', *, *, #8303, .T. ) ;
#10010=CIRCLE ( 'NONE', #5019, 27.00000000002699707 ) ;
#10012=CIRCLE ( 'NONE', #3028, 20.24900000002024925 ) ;
#10015=CARTESIAN_POINT ( 'NONE',  ( 4.999999999999999112, 0.000000000000000000, 0.000000000000000000 ) ) ;
#10020=ORIENTED_EDGE ( 'NONE', *, *, #9960, .T. ) ;
#10022=ORIENTED_EDGE ( 'NONE', *, *, #189, .F. ) ;
#10023=FACE_OUTER_BOUND ( 'NONE', #6040, .T. ) ;
#10026=VECTOR ( 'NONE', #10768, 1000.000000000000000 ) ;
#10032=DIRECTION ( 'NONE',  ( -1.000000000000000000, 0.000000000000000000, 0.000000000000000000 ) ) ;
#10038=VECTOR ( 'NONE', #8582, 1000.000000000000000 ) ;
#10042=VERTEX_POINT ( 'NONE', #890 ) ;
#10045=AXIS2_PLACEMENT_3D ( 'NONE', #5, #3832, #1954 ) ;
#10050=DIRECTION ( 'NONE',  ( 0.000000000000000000, -0.9238795325112827417, -0.3826834323650997738 ) ) ;
#10053=VERTEX_POINT ( 'NONE', #4892 ) ;
#10064=ORIENTED_EDGE ( 'NONE', *, *, #60, .F. ) ;
#10068=CARTESIAN_POINT ( 'NONE',  ( 4.999999999999999112, 0.000000000000000000, 0.000000000000000000 ) ) ;
#10076=CYLINDRICAL_SURFACE ( 'NONE', #6005, 27.00000000002699707 ) ;
#10081=ORIENTED_EDGE ( 'NONE', *, *, #10876, .F. ) ;
#10083=EDGE_CURVE ( 'NONE', #11670, #6904, #11827, .T. ) ;
#10086=CARTESIAN_POINT ( 'NONE',  ( 4.999999999999999112, 22.37914155802281257, 2.791921004064645384 ) ) ;
#10091=LINE ( 'NONE', #6280, #6196 ) ;
#10095=EDGE_LOOP ( 'NONE', ( #8550, #9930, #9096, #390 ) ) ;
#10103=CARTESIAN_POINT ( 'NONE',  ( 0.000000000000000000, -22.37914155802287297, 2.791921004064167544 ) ) ;
#10113=LINE ( 'NONE', #5236, #817 ) ;
#10115=ORIENTED_EDGE ( 'NONE', *, *, #5543, .F. ) ;
#10118=EDGE_CURVE ( 'NONE', #9337, #10885, #9855, .T. ) ;
#10126=DIRECTION ( 'NONE',  ( 0.000000000000000000, 0.7071067811865487940, -0.7071067811865462405 ) ) ;
#10129=EDGE_CURVE ( 'NONE', #10139, #12254, #2652, .T. ) ;
#10130=CARTESIAN_POINT ( 'NONE',  ( 4.999999999999999112, 21.74405275335766419, -5.984728032764733641 ) ) ;
#10131=FACE_OUTER_BOUND ( 'NONE', #3123, .T. ) ;
#10132=ADVANCED_FACE ( 'NONE', ( #7900 ), #3145, .T. ) ;
#10136=CARTESIAN_POINT ( 'NONE',  ( 4.999999999999999112, 22.83261415639523051, -14.41081992069284645 ) ) ;
#10137=EDGE_LOOP ( 'NONE', ( #10986, #3800, #1778, #578 ) ) ;
#10139=VERTEX_POINT ( 'NONE', #6952 ) ;
#10143=CARTESIAN_POINT ( 'NONE',  ( 4.999999999999999112, 22.37914155802285876, -2.791921004064323864 ) ) ;
#10149=DIRECTION ( 'NONE',  ( 0.000000000000000000, 0.000000000000000000, 1.000000000000000000 ) ) ;
#10154=EDGE_CURVE ( 'NONE', #12088, #1163, #10756, .T. ) ;
#10157=LINE ( 'NONE', #6411, #816 ) ;
#10158=LINE ( 'NONE', #5479, #2434 ) ;
#10159=CARTESIAN_POINT ( 'NONE',  ( 4.999999999999999112, 0.000000000000000000, 0.000000000000000000 ) ) ;
#10162=ORIENTED_EDGE ( 'NONE', *, *, #4195, .T. ) ;
#10165=FACE_OUTER_BOUND ( 'NONE', #1672, .T. ) ;
#10169=DIRECTION ( 'NONE',  ( 0.000000000000000000, 0.000000000000000000, -1.000000000000000000 ) ) ;
#10170=AXIS2_PLACEMENT_3D ( 'NONE', #1957, #8655, #3711 ) ;
#10174=CARTESIAN_POINT ( 'NONE',  ( 0.000000000000000000, -22.37914155802283034, -2.791921004064479739 ) ) ;
#10176=CYLINDRICAL_SURFACE ( 'NONE', #904, 9.600000000009600853 ) ;
#10178=DIRECTION ( 'NONE',  ( -1.000000000000000000, -0.000000000000000000, 0.000000000000000000 ) ) ;
#10182=DIRECTION ( 'NONE',  ( 0.000000000000000000, 0.000000000000000000, 1.000000000000000000 ) ) ;
#10193=EDGE_CURVE ( 'NONE', #4722, #9598, #6867, .T. ) ;
#10194=ORIENTED_EDGE ( 'NONE', *, *, #8976, .T. ) ;
#10196=EDGE_CURVE ( 'NONE', #10053, #7220, #2192, .T. ) ;
#10199=CIRCLE ( 'NONE', #5820, 20.24900000002025280 ) ;
#10204=DIRECTION ( 'NONE',  ( -1.000000000000000000, -0.000000000000000000, -0.000000000000000000 ) ) ;
#10206=CYLINDRICAL_SURFACE ( 'NONE', #10949, 27.00000000002699707 ) ;
#10207=DIRECTION ( 'NONE',  ( -1.000000000000000000, -0.000000000000000000, 0.000000000000000000 ) ) ;
#10211=CARTESIAN_POINT ( 'NONE',  ( 4.999999999999999112, 6.283573709965309284, 19.24938187143298052 ) ) ;
#10214=VECTOR ( 'NONE', #9747, 1000.000000000000000 ) ;
#10220=CARTESIAN_POINT ( 'NONE',  ( 4.999999999999999112, -18.05452603534171985, 9.168210874537514599 ) ) ;
#10243=EDGE_CURVE ( 'NONE', #4464, #1857, #6054, .T. ) ;
#10246=DIRECTION ( 'NONE',  ( -1.000000000000000000, 0.000000000000000000, 0.000000000000000000 ) ) ;
#10247=AXIS2_PLACEMENT_3D ( 'NONE', #1782, #9420, #4670 ) ;
#10248=DIRECTION ( 'NONE',  ( 0.000000000000000000, 0.000000000000000000, 1.000000000000000000 ) ) ;
#10255=CARTESIAN_POINT ( 'NONE',  ( 4.999999999999999112, 0.000000000000000000, 0.000000000000000000 ) ) ;
#10257=ORIENTED_EDGE ( 'NONE', *, *, #4003, .F. ) ;
#10276=CYLINDRICAL_SURFACE ( 'NONE', #3621, 9.600000000009600853 ) ;
#10278=AXIS2_PLACEMENT_3D ( 'NONE', #6570, #665, #10375 ) ;
#10280=DIRECTION ( 'NONE',  ( -1.000000000000000000, 0.000000000000000000, 0.000000000000000000 ) ) ;
#10281=ORIENTED_EDGE ( 'NONE', *, *, #12024, .F. ) ;
#10282=ORIENTED_EDGE ( 'NONE', *, *, #10828, .T. ) ;
#10284=ADVANCED_FACE ( 'NONE', ( #621 ), #5507, .T. ) ;
#10286=EDGE_CURVE ( 'NONE', #7642, #4373, #175, .T. ) ;
#10288=CARTESIAN_POINT ( 'NONE',  ( 4.999999999999999112, -11.14352537685188338, 19.60720892790249081 ) ) ;
#10297=DIRECTION ( 'NONE',  ( 0.000000000000000000, 0.000000000000000000, -1.000000000000000000 ) ) ;
#10299=FILL_AREA_STYLE ('',( #925 ) ) ;
#10308=DIRECTION ( 'NONE',  ( 0.000000000000000000, 0.9238795325112876267, -0.3826834323650873393 ) ) ;
#10310=ORIENTED_EDGE ( 'NONE', *, *, #1367, .T. ) ;
#10330=CYLINDRICAL_SURFACE ( 'NONE', #2007, 20.24900000002024569 ) ;
#10332=LINE ( 'NONE', #768, #6239 ) ;
#10336=FACE_OUTER_BOUND ( 'NONE', #7173, .T. ) ;
#10338=CYLINDRICAL_SURFACE ( 'NONE', #10247, 9.600000000009600853 ) ;
#10345=VECTOR ( 'NONE', #3814, 1000.000000000000000 ) ;
#10346=EDGE_CURVE ( 'NONE', #8188, #908, #12238, .T. ) ;
#10348=AXIS2_PLACEMENT_3D ( 'NONE', #7215, #11936, #3338 ) ;
#10353=CARTESIAN_POINT ( 'NONE',  ( 4.999999999999999112, 0.000000000000000000, 0.000000000000000000 ) ) ;
#10354=ORIENTED_EDGE ( 'NONE', *, *, #1585, .F. ) ;
#10364=AXIS2_PLACEMENT_3D ( 'NONE', #44, #104, #3976 ) ;
#10365=VECTOR ( 'NONE', #9132, 1000.000000000000000 ) ;
#10375=DIRECTION ( 'NONE',  ( 0.000000000000000000, -0.7071067811865536790, 0.7071067811865413555 ) ) ;
#10381=VECTOR ( 'NONE', #8394, 1000.000000000000000 ) ;
#10382=DIRECTION ( 'NONE',  ( -1.000000000000000000, -0.000000000000000000, 0.000000000000000000 ) ) ;
#10385=CIRCLE ( 'NONE', #10983, 9.600000000009602630 ) ;
#10386=DIRECTION ( 'NONE',  ( -1.000000000000000000, 0.000000000000000000, -0.000000000000000000 ) ) ;
#10389=CARTESIAN_POINT ( 'NONE',  ( 4.999999999999997335, 0.000000000000000000, 5.000000000000000000 ) ) ;
#10400=DIRECTION ( 'NONE',  ( -1.000000000000000000, 0.000000000000000000, 0.000000000000000000 ) ) ;
#10402=AXIS2_PLACEMENT_3D ( 'NONE', #4975, #3866, #8802 ) ;
#10408=ORIENTED_EDGE ( 'NONE', *, *, #3181, .F. ) ;
#10410=ORIENTED_EDGE ( 'NONE', *, *, #1367, .F. ) ;
#10412=CYLINDRICAL_SURFACE ( 'NONE', #1772, 20.24900000002024569 ) ;
#10413=CIRCLE ( 'NONE', #5840, 9.600000000009600853 ) ;
#10418=VERTEX_POINT ( 'NONE', #7640 ) ;
#10422=EDGE_CURVE ( 'NONE', #7570, #7924, #8566, .T. ) ;
#10425=AXIS2_PLACEMENT_3D ( 'NONE', #11317, #5645, #3648 ) ;
#10429=AXIS2_PLACEMENT_3D ( 'NONE', #6398, #10204, #5397 ) ;
#10430=ORIENTED_EDGE ( 'NONE', *, *, #2158, .T. ) ;
#10438=AXIS2_PLACEMENT_3D ( 'NONE', #2134, #9770, #1193 ) ;
#10440=DIRECTION ( 'NONE',  ( 0.000000000000000000, 0.000000000000000000, 1.000000000000000000 ) ) ;
#10447=EDGE_CURVE ( 'NONE', #1740, #11007, #3747, .T. ) ;
#10454=CYLINDRICAL_SURFACE ( 'NONE', #1815, 27.00000000002699707 ) ;
#10464=ORIENTED_EDGE ( 'NONE', *, *, #9578, .T. ) ;
#10465=CIRCLE ( 'NONE', #3679, 9.600000000009602630 ) ;
#10467=LINE ( 'NONE', #3961, #9561 ) ;
#10471=ORIENTED_EDGE ( 'NONE', *, *, #2613, .T. ) ;
#10481=VERTEX_POINT ( 'NONE', #11436 ) ;
#10486=ORIENTED_EDGE ( 'NONE', *, *, #7462, .F. ) ;
#10491=EDGE_LOOP ( 'NONE', ( #10514, #7423, #5298, #1015, #2541, #4593, #10115, #3429, #8850, #1043, #1735, #9011, #7337, #9289, #1295, #2706, #9399, #10991, #3918, #3838, #10837, #6350, #7469, #7315, #7074, #1153, #7676, #9316, #7732, #95, #697, #6115, #157, #6258, #1316, #6383, #4685, #6790, #7466, #6987, #6344, #9631, #9571, #11352, #6957, #7359, #13, #10486, #12341, #9717, #5841, #10758, #9731, #2777, #10081, #7905, #9729, #6748, #43, #4797, #6386, #3669, #6601, #9516, #3693, #9199, #6553, #10601, #9674 ) ) ;
#10495=ADVANCED_FACE ( 'NONE', ( #9641 ), #1067, .T. ) ;
#10499=FACE_OUTER_BOUND ( 'NONE', #6621, .T. ) ;
#10501=DIRECTION ( 'NONE',  ( 0.000000000000000000, 0.000000000000000000, 1.000000000000000000 ) ) ;
#10504=CARTESIAN_POINT ( 'NONE',  ( 0.000000000000000000, -18.05452603534159195, -9.168210874537770394 ) ) ;
#10513=DIRECTION ( 'NONE',  ( -1.000000000000000000, 0.000000000000000000, 0.000000000000000000 ) ) ;
#10514=ORIENTED_EDGE ( 'NONE', *, *, #11654, .F. ) ;
#10515=CARTESIAN_POINT ( 'NONE',  ( 0.000000000000000000, 21.74405275335758247, 5.984728032765037398 ) ) ;
#10518=CARTESIAN_POINT ( 'NONE',  ( 2.499999999999999556, -22.05152472667140984, 15.57980286237464895 ) ) ;
#10525=DIRECTION ( 'NONE',  ( -1.000000000000000000, -0.000000000000000000, -0.000000000000000000 ) ) ;
#10526=CARTESIAN_POINT ( 'NONE',  ( 0.000000000000000000, 4.769696007084728073, 1.500000000000000000 ) ) ;
#10528=ORIENTED_EDGE ( 'NONE', *, *, #3642, .F. ) ;
#10531=CARTESIAN_POINT ( 'NONE',  ( 0.000000000000000000, 0.000000000000000000, 0.000000000000000000 ) ) ;
#10533=ORIENTED_EDGE ( 'NONE', *, *, #11974, .T. ) ;
#10540=CARTESIAN_POINT ( 'NONE',  ( 0.000000000000000000, 0.000000000000000000, 0.000000000000000000 ) ) ;
#10541=DIRECTION ( 'NONE',  ( 0.000000000000000000, 0.000000000000000000, 1.000000000000000000 ) ) ;
#10544=VERTEX_POINT ( 'NONE', #3313 ) ;
#10545=( NAMED_UNIT ( * ) PLANE_ANGLE_UNIT ( ) SI_UNIT ( $, .RADIAN. ) );
#10547=AXIS2_PLACEMENT_3D ( 'NONE', #492, #4301, #11062 ) ;
#10552=DIRECTION ( 'NONE',  ( -1.000000000000000000, -0.000000000000000000, 0.000000000000000000 ) ) ;
#10554=VECTOR ( 'NONE', #7888, 1000.000000000000000 ) ;
#10560=DIRECTION ( 'NONE',  ( 0.000000000000000000, 0.000000000000000000, 1.000000000000000000 ) ) ;
#10563=SHAPE_REPRESENTATION ( 'spur gear_iso_ISO - Spur gear 3M 16T 20PA 5FW ---S16A75H50L10.0S1', ( #6056 ), #3048 ) ;
#10572=CIRCLE ( 'NONE', #356, 9.600000000009600853 ) ;
#10574=EDGE_CURVE ( 'NONE', #5514, #9474, #10922, .T. ) ;
#10577=CIRCLE ( 'NONE', #201, 20.24900000002024569 ) ;
#10578=ORIENTED_EDGE ( 'NONE', *, *, #7462, .T. ) ;
#10579=DIRECTION ( 'NONE',  ( -1.000000000000000000, -0.000000000000000000, 0.000000000000000000 ) ) ;
#10582=ADVANCED_FACE ( 'NONE', ( #9753 ), #11681, .T. ) ;
#10585=CARTESIAN_POINT ( 'NONE',  ( 0.000000000000000000, 6.799999999999999822, -1.500000000000000000 ) ) ;
#10588=DIRECTION ( 'NONE',  ( -1.000000000000000000, 0.000000000000000000, 0.000000000000000000 ) ) ;
#10592=ORIENTED_EDGE ( 'NONE', *, *, #9149, .T. ) ;
#10594=EDGE_CURVE ( 'NONE', #2589, #10481, #1768, .T. ) ;
#10600=EDGE_CURVE ( 'NONE', #1066, #11750, #4767, .T. ) ;
#10601=ORIENTED_EDGE ( 'NONE', *, *, #3739, .F. ) ;
#10605=DIRECTION ( 'NONE',  ( -1.000000000000000000, -0.000000000000000000, -0.000000000000000000 ) ) ;
#10617=ORIENTED_EDGE ( 'NONE', *, *, #8976, .F. ) ;
#10630=EDGE_CURVE ( 'NONE', #138, #11506, #6777, .T. ) ;
#10633=CARTESIAN_POINT ( 'NONE',  ( 4.999999999999999112, 11.14352537685202016, -19.60720892790241265 ) ) ;
#10641=ORIENTED_EDGE ( 'NONE', *, *, #8994, .T. ) ;
#10642=AXIS2_PLACEMENT_3D ( 'NONE', #10143, #1644, #1575 ) ;
#10644=AXIS2_PLACEMENT_3D ( 'NONE', #6081, #263, #9947 ) ;
#10645=CARTESIAN_POINT ( 'NONE',  ( 4.999999999999999112, -22.37914155802283034, -2.791921004064479739 ) ) ;
#10650=ORIENTED_EDGE ( 'NONE', *, *, #8530, .T. ) ;
#10663=LINE ( 'NONE', #5964, #10816 ) ;
#10665=VERTEX_POINT ( 'NONE', #7067 ) ;
#10670=EDGE_CURVE ( 'NONE', #10919, #6904, #7178, .T. ) ;
#10676=EDGE_CURVE ( 'NONE', #10544, #4720, #11940, .T. ) ;
#10680=ORIENTED_EDGE ( 'NONE', *, *, #6691, .T. ) ;
#10686=ORIENTED_EDGE ( 'NONE', *, *, #11112, .T. ) ;
#10711=CARTESIAN_POINT ( 'NONE',  ( 4.999999999999999112, 19.24938187143296275, 6.283573709965379450 ) ) ;
#10721=ORIENTED_EDGE ( 'NONE', *, *, #3118, .T. ) ;
#10728=DIRECTION ( 'NONE',  ( 0.000000000000000000, 0.000000000000000000, -1.000000000000000000 ) ) ;
#10731=ORIENTED_EDGE ( 'NONE', *, *, #4539, .T. ) ;
#10740=ORIENTED_EDGE ( 'NONE', *, *, #9033, .T. ) ;
#10742=DIRECTION ( 'NONE',  ( 0.000000000000000000, 0.000000000000000000, -1.000000000000000000 ) ) ;
#10743=ORIENTED_EDGE ( 'NONE', *, *, #1493, .F. ) ;
#10749=ORIENTED_EDGE ( 'NONE', *, *, #10600, .T. ) ;
#10752=VECTOR ( 'NONE', #301, 1000.000000000000000 ) ;
#10756=LINE ( 'NONE', #9840, #2063 ) ;
#10758=ORIENTED_EDGE ( 'NONE', *, *, #10129, .F. ) ;
#10761=DIRECTION ( 'NONE',  ( 0.000000000000000000, -0.3826834323650971648, 0.9238795325112837409 ) ) ;
#10768=DIRECTION ( 'NONE',  ( 1.000000000000000000, -0.000000000000000000, -0.000000000000000000 ) ) ;
#10769=CIRCLE ( 'NONE', #11165, 9.600000000009600853 ) ;
#10772=CIRCLE ( 'NONE', #4375, 20.24900000002024569 ) ;
#10785=DIRECTION ( 'NONE',  ( 0.000000000000000000, 0.000000000000000000, 1.000000000000000000 ) ) ;
#10790=ORIENTED_EDGE ( 'NONE', *, *, #10574, .T. ) ;
#10800=EDGE_CURVE ( 'NONE', #4621, #11283, #5975, .T. ) ;
#10801=ORIENTED_EDGE ( 'NONE', *, *, #10154, .F. ) ;
#10803=DIRECTION ( 'NONE',  ( 1.000000000000000000, 0.000000000000000000, 0.000000000000000000 ) ) ;
#10816=VECTOR ( 'NONE', #6672, 1000.000000000000000 ) ;
#10826=DIRECTION ( 'NONE',  ( -1.000000000000000000, -0.000000000000000000, 0.000000000000000000 ) ) ;
#10827=CARTESIAN_POINT ( 'NONE',  ( 0.000000000000000000, 15.37949036966230132, -13.17168466712912434 ) ) ;
#10828=EDGE_CURVE ( 'NONE', #3326, #4782, #8374, .T. ) ;
#10837=ORIENTED_EDGE ( 'NONE', *, *, #10968, .F. ) ;
#10846=CARTESIAN_POINT ( 'NONE',  ( 0.000000000000000000, 6.799999999999999822, 0.000000000000000000 ) ) ;
#10848=ORIENTED_EDGE ( 'NONE', *, *, #11124, .F. ) ;
#10854=DIRECTION ( 'NONE',  ( -1.000000000000000000, 0.000000000000000000, -0.000000000000000000 ) ) ;
#10865=CARTESIAN_POINT ( 'NONE',  ( 0.000000000000000000, 22.37914155802285876, -2.791921004064323864 ) ) ;
#10867=CYLINDRICAL_SURFACE ( 'NONE', #6008, 9.600000000009600853 ) ;
#10868=VERTEX_POINT ( 'NONE', #12290 ) ;
#10869=DIRECTION ( 'NONE',  ( 0.000000000000000000, 0.000000000000000000, 1.000000000000000000 ) ) ;
#10871=CARTESIAN_POINT ( 'NONE',  ( 0.000000000000000000, 22.05152472667151642, -15.57980286237449619 ) ) ;
#10875=FACE_OUTER_BOUND ( 'NONE', #6907, .T. ) ;
#10876=EDGE_CURVE ( 'NONE', #6875, #4331, #4970, .T. ) ;
#10877=EDGE_LOOP ( 'NONE', ( #3615, #10902, #11920, #7523 ) ) ;
#10885=VERTEX_POINT ( 'NONE', #4799 ) ;
#10894=EDGE_CURVE ( 'NONE', #10885, #11449, #1933, .T. ) ;
#10900=ORIENTED_EDGE ( 'NONE', *, *, #9376, .T. ) ;
#10902=ORIENTED_EDGE ( 'NONE', *, *, #4148, .T. ) ;
#10905=CARTESIAN_POINT ( 'NONE',  ( 4.999999999999999112, 21.74405275335758247, 5.984728032765037398 ) ) ;
#10917=CARTESIAN_POINT ( 'NONE',  ( -10.00000000000000000, 0.000000000000000000, 0.000000000000000000 ) ) ;
#10919=VERTEX_POINT ( 'NONE', #9554 ) ;
#10920=DIRECTION ( 'NONE',  ( -1.000000000000000000, -0.000000000000000000, 0.000000000000000000 ) ) ;
#10922=LINE ( 'NONE', #2121, #10554 ) ;
#10925=DIRECTION ( 'NONE',  ( -1.000000000000000000, -0.000000000000000000, 0.000000000000000000 ) ) ;
#10932=DIRECTION ( 'NONE',  ( -1.000000000000000000, -0.000000000000000000, -0.000000000000000000 ) ) ;
#10935=ADVANCED_FACE ( 'NONE', ( #4681 ), #50, .T. ) ;
#10936=CARTESIAN_POINT ( 'NONE',  ( 0.000000000000000000, 19.24938187143295920, 6.283573709965377674 ) ) ;
#10944=AXIS2_PLACEMENT_3D ( 'NONE', #8153, #637, #11018 ) ;
#10947=CYLINDRICAL_SURFACE ( 'NONE', #11227, 9.600000000009602630 ) ;
#10948=CARTESIAN_POINT ( 'NONE',  ( 0.000000000000000000, -5.955107813822308138, -26.33508479058327367 ) ) ;
#10949=AXIS2_PLACEMENT_3D ( 'NONE', #8218, #1707, #5338 ) ;
#10957=ORIENTED_EDGE ( 'NONE', *, *, #6033, .F. ) ;
#10960=AXIS2_PLACEMENT_3D ( 'NONE', #12347, #3870, #2795 ) ;
#10961=DIRECTION ( 'NONE',  ( 0.000000000000000000, 0.000000000000000000, 1.000000000000000000 ) ) ;
#10967=ORIENTED_EDGE ( 'NONE', *, *, #5785, .T. ) ;
#10968=EDGE_CURVE ( 'NONE', #4264, #8081, #1578, .T. ) ;
#10969=ADVANCED_FACE ( 'NONE', ( #4868 ), #3926, .T. ) ;
#10970=CARTESIAN_POINT ( 'NONE',  ( 4.999999999999999112, 5.984728032764962791, 21.74405275335760379 ) ) ;
#10975=VERTEX_POINT ( 'NONE', #11944 ) ;
#10982=EDGE_CURVE ( 'NONE', #3672, #7335, #6370, .T. ) ;
#10983=AXIS2_PLACEMENT_3D ( 'NONE', #3071, #11435, #8565 ) ;
#10986=ORIENTED_EDGE ( 'NONE', *, *, #8783, .T. ) ;
#10989=CARTESIAN_POINT ( 'NONE',  ( 4.999999999999999112, -17.79862902732255137, -13.85025647830076245 ) ) ;
#10991=ORIENTED_EDGE ( 'NONE', *, *, #1399, .F. ) ;
#10996=CIRCLE ( 'NONE', #5018, 27.00000000002699707 ) ;
#11003=VERTEX_POINT ( 'NONE', #7102 ) ;
#11005=CARTESIAN_POINT ( 'NONE',  ( 0.000000000000000000, 0.000000000000000000, 0.000000000000000000 ) ) ;
#11007=VERTEX_POINT ( 'NONE', #6286 ) ;
#11012=CIRCLE ( 'NONE', #9638, 27.00000000002699707 ) ;
#11016=VERTEX_POINT ( 'NONE', #9965 ) ;
#11018=DIRECTION ( 'NONE',  ( 0.000000000000000000, 0.9238795325112878487, -0.3826834323650872283 ) ) ;
#11032=CIRCLE ( 'NONE', #1846, 27.00000000002699707 ) ;
#11036=DIRECTION ( 'NONE',  ( 0.000000000000000000, 0.3826834323650905589, -0.9238795325112864054 ) ) ;
#11037=DIRECTION ( 'NONE',  ( -1.000000000000000000, 0.000000000000000000, 0.000000000000000000 ) ) ;
#11039=CARTESIAN_POINT ( 'NONE',  ( 0.000000000000000000, -9.168210874537708222, 18.05452603534162748 ) ) ;
#11040=DIRECTION ( 'NONE',  ( 0.000000000000000000, 0.000000000000000000, 1.000000000000000000 ) ) ;
#11051=EDGE_CURVE ( 'NONE', #3907, #1528, #11087, .T. ) ;
#11053=VERTEX_POINT ( 'NONE', #9109 ) ;
#11058=ORIENTED_EDGE ( 'NONE', *, *, #9531, .T. ) ;
#11062=DIRECTION ( 'NONE',  ( 0.000000000000000000, 0.000000000000000000, -1.000000000000000000 ) ) ;
#11065=DIRECTION ( 'NONE',  ( -1.000000000000000000, -0.000000000000000000, -0.000000000000000000 ) ) ;
#11082=CARTESIAN_POINT ( 'NONE',  ( 4.999999999999999112, -13.85025647830044271, -17.79862902732279650 ) ) ;
#11083=LINE ( 'NONE', #3393, #2437 ) ;
#11085=FACE_OUTER_BOUND ( 'NONE', #10877, .T. ) ;
#11087=LINE ( 'NONE', #3470, #2221 ) ;
#11093=CARTESIAN_POINT ( 'NONE',  ( 0.000000000000000000, -21.74405275335762155, 5.984728032764886407 ) ) ;
#11095=CARTESIAN_POINT ( 'NONE',  ( 4.999999999999999112, 0.000000000000000000, 0.000000000000000000 ) ) ;
#11096=ORIENTED_EDGE ( 'NONE', *, *, #119, .T. ) ;
#11098=ORIENTED_EDGE ( 'NONE', *, *, #2888, .T. ) ;
#11104=ORIENTED_EDGE ( 'NONE', *, *, #4875, .T. ) ;
#11112=EDGE_CURVE ( 'NONE', #11003, #4243, #10010, .T. ) ;
#11115=CARTESIAN_POINT ( 'NONE',  ( 0.000000000000000000, 0.000000000000000000, 0.000000000000000000 ) ) ;
#11121=ORIENTED_EDGE ( 'NONE', *, *, #9258, .T. ) ;
#11122=VERTEX_POINT ( 'NONE', #9222 ) ;
#11124=EDGE_CURVE ( 'NONE', #1740, #4492, #8472, .T. ) ;
#11128=ORIENTED_EDGE ( 'NONE', *, *, #10346, .T. ) ;
#11133=LINE ( 'NONE', #8280, #11933 ) ;
#11136=DIRECTION ( 'NONE',  ( 0.000000000000000000, 0.000000000000000000, 1.000000000000000000 ) ) ;
#11149=FACE_OUTER_BOUND ( 'NONE', #8840, .T. ) ;
#11150=DIRECTION ( 'NONE',  ( 0.000000000000000000, 0.3826834323650841752, 0.9238795325112890700 ) ) ;
#11153=DIRECTION ( 'NONE',  ( -1.000000000000000000, 0.000000000000000000, -0.000000000000000000 ) ) ;
#11154=EDGE_LOOP ( 'NONE', ( #3153, #9881, #4180, #9583 ) ) ;
#11161=FACE_OUTER_BOUND ( 'NONE', #3742, .T. ) ;
#11162=VECTOR ( 'NONE', #6047, 1000.000000000000000 ) ;
#11165=AXIS2_PLACEMENT_3D ( 'NONE', #5761, #9585, #8525 ) ;
#11172=LINE ( 'NONE', #1500, #10365 ) ;
#11177=EDGE_CURVE ( 'NONE', #7435, #10418, #6471, .T. ) ;
#11184=CYLINDRICAL_SURFACE ( 'NONE', #8634, 20.24900000002024569 ) ;
#11190=VECTOR ( 'NONE', #5072, 1000.000000000000000 ) ;
#11195=AXIS2_PLACEMENT_3D ( 'NONE', #1715, #6480, #9296 ) ;
#11198=LINE ( 'NONE', #4513, #2397 ) ;
#11204=CARTESIAN_POINT ( 'NONE',  ( 0.000000000000000000, 20.18872947935930995, 1.561154383803294410 ) ) ;
#11209=VERTEX_POINT ( 'NONE', #5400 ) ;
#11210=AXIS2_PLACEMENT_3D ( 'NONE', #4265, #9032, #323 ) ;
#11215=CYLINDRICAL_SURFACE ( 'NONE', #1195, 9.600000000009600853 ) ;
#11218=DIRECTION ( 'NONE',  ( 0.000000000000000000, 0.000000000000000000, -1.000000000000000000 ) ) ;
#11223=CARTESIAN_POINT ( 'NONE',  ( 4.999999999999999112, -26.33508479058316354, -5.955107813822782425 ) ) ;
#11227=AXIS2_PLACEMENT_3D ( 'NONE', #6036, #4202, #11702 ) ;
#11231=CIRCLE ( 'NONE', #1459, 27.00000000002699707 ) ;
#11242=CARTESIAN_POINT ( 'NONE',  ( 0.000000000000000000, -4.576198416197066798, -26.60936692326695407 ) ) ;
#11247=DIRECTION ( 'NONE',  ( 0.000000000000000000, 0.000000000000000000, 1.000000000000000000 ) ) ;
#11250=ORIENTED_EDGE ( 'NONE', *, *, #5750, .T. ) ;
#11255=FACE_OUTER_BOUND ( 'NONE', #3134, .T. ) ;
#11261=CARTESIAN_POINT ( 'NONE',  ( 4.999999999999999112, 6.283573709965571297, -19.24938187143289881 ) ) ;
#11262=ORIENTED_EDGE ( 'NONE', *, *, #2698, .F. ) ;
#11263=CARTESIAN_POINT ( 'NONE',  ( 4.999999999999999112, 0.000000000000000000, 0.000000000000000000 ) ) ;
#11265=ORIENTED_EDGE ( 'NONE', *, *, #3267, .T. ) ;
#11271=EDGE_CURVE ( 'NONE', #11670, #6322, #25, .T. ) ;
#11273=VERTEX_POINT ( 'NONE', #9773 ) ;
#11276=FACE_OUTER_BOUND ( 'NONE', #12240, .T. ) ;
#11283=VERTEX_POINT ( 'NONE', #7665 ) ;
#11291=LINE ( 'NONE', #9183, #206 ) ;
#11297=CARTESIAN_POINT ( 'NONE',  ( 50.00005079999999680, 4.769696007084728073, -1.500000000000000000 ) ) ;
#11302=DIRECTION ( 'NONE',  ( 0.000000000000000000, -6.866613759067993855E-15, 1.000000000000000000 ) ) ;
#11306=VERTEX_POINT ( 'NONE', #8773 ) ;
#11307=ORIENTED_EDGE ( 'NONE', *, *, #4003, .T. ) ;
#11312=ORIENTED_EDGE ( 'NONE', *, *, #6020, .T. ) ;
#11317=CARTESIAN_POINT ( 'NONE',  ( 4.999999999999999112, 0.000000000000000000, 0.000000000000000000 ) ) ;
#11320=DIRECTION ( 'NONE',  ( -1.000000000000000000, 0.000000000000000000, -0.000000000000000000 ) ) ;
#11334=ORIENTED_EDGE ( 'NONE', *, *, #2272, .T. ) ;
#11338=DIRECTION ( 'NONE',  ( 0.000000000000000000, -0.3826834323650774028, -0.9238795325112918455 ) ) ;
#11339=CIRCLE ( 'NONE', #2356, 9.600000000009599077 ) ;
#11352=ORIENTED_EDGE ( 'NONE', *, *, #2670, .F. ) ;
#11356=CARTESIAN_POINT ( 'NONE',  ( 50.00005079999999680, 6.123233995736766282E-16, -5.000000000000000000 ) ) ;
#11357=ORIENTED_EDGE ( 'NONE', *, *, #5702, .F. ) ;
#11358=CARTESIAN_POINT ( 'NONE',  ( 4.999999999999999112, -13.17168466712939257, 15.37949036966207039 ) ) ;
#11367=CARTESIAN_POINT ( 'NONE',  ( 4.999999999999999112, 0.000000000000000000, 0.000000000000000000 ) ) ;
#11370=CIRCLE ( 'NONE', #9991, 9.600000000009600853 ) ;
#11373=LINE ( 'NONE', #9463, #2993 ) ;
#11375=EDGE_CURVE ( 'NONE', #11209, #1819, #2417, .T. ) ;
#11380=AXIS2_PLACEMENT_3D ( 'NONE', #7561, #6506, #10248 ) ;
#11387=DIRECTION ( 'NONE',  ( -1.000000000000000000, 0.000000000000000000, 0.000000000000000000 ) ) ;
#11388=UNCERTAINTY_MEASURE_WITH_UNIT (LENGTH_MEASURE( 1.000000000000000082E-05 ), #12161, 'distance_accuracy_value', 'NONE');
#11400=ORIENTED_EDGE ( 'NONE', *, *, #9544, .T. ) ;
#11401=ORIENTED_EDGE ( 'NONE', *, *, #8398, .F. ) ;
#11403=CIRCLE ( 'NONE', #4024, 27.00000000002699707 ) ;
#11412=CIRCLE ( 'NONE', #1837, 9.600000000009602630 ) ;
#11413=CIRCLE ( 'NONE', #634, 9.600000000009599077 ) ;
#11421=EDGE_LOOP ( 'NONE', ( #9141, #347, #1086, #6555 ) ) ;
#11423=AXIS2_PLACEMENT_3D ( 'NONE', #11263, #9284, #2700 ) ;
#11427=CIRCLE ( 'NONE', #3247, 9.600000000009600853 ) ;
#11428=ORIENTED_EDGE ( 'NONE', *, *, #9679, .T. ) ;
#11429=CARTESIAN_POINT ( 'NONE',  ( 4.999999999999999112, 20.18872947935930995, 1.561154383803294410 ) ) ;
#11435=DIRECTION ( 'NONE',  ( -1.000000000000000000, 0.000000000000000000, 0.000000000000000000 ) ) ;
#11436=CARTESIAN_POINT ( 'NONE',  ( 0.000000000000000000, 26.33508479058329499, -5.955107813822217544 ) ) ;
#11439=DIRECTION ( 'NONE',  ( -1.000000000000000000, -0.000000000000000000, -0.000000000000000000 ) ) ;
#11445=DIRECTION ( 'NONE',  ( 0.000000000000000000, 0.000000000000000000, -1.000000000000000000 ) ) ;
#11447=DIRECTION ( 'NONE',  ( 0.000000000000000000, 1.000000000000000000, 3.491481338843133750E-15 ) ) ;
#11449=VERTEX_POINT ( 'NONE', #11818 ) ;
#11455=CARTESIAN_POINT ( 'NONE',  ( 4.999999999999999112, 0.000000000000000000, 0.000000000000000000 ) ) ;
#11456=VERTEX_POINT ( 'NONE', #9899 ) ;
#11465=CIRCLE ( 'NONE', #5892, 9.600000000009600853 ) ;
#11466=EDGE_LOOP ( 'NONE', ( #1959, #3312, #9851, #9328 ) ) ;
#11471=EDGE_LOOP ( 'NONE', ( #5986, #10282, #7588, #1372 ) ) ;
#11474=DIRECTION ( 'NONE',  ( -1.000000000000000000, 0.000000000000000000, -0.000000000000000000 ) ) ;
#11482=SHAPE_REPRESENTATION_RELATIONSHIP ( 'NONE' , 'NONE' ,  #10563, #8868 ) ;
#11492=EDGE_CURVE ( 'NONE', #7335, #7692, #831, .T. ) ;
#11495=FACE_OUTER_BOUND ( 'NONE', #5289, .T. ) ;
#11497=VERTEX_POINT ( 'NONE', #6085 ) ;
#11499=LINE ( 'NONE', #6655, #8208 ) ;
#11506=VERTEX_POINT ( 'NONE', #1266 ) ;
#11513=EDGE_CURVE ( 'NONE', #7220, #11850, #4837, .T. ) ;
#11531=DIRECTION ( 'NONE',  ( -1.000000000000000000, 0.000000000000000000, 0.000000000000000000 ) ) ;
#11537=CIRCLE ( 'NONE', #12338, 20.24900000002024569 ) ;
#11539=ORIENTED_EDGE ( 'NONE', *, *, #2489, .F. ) ;
#11542=CARTESIAN_POINT ( 'NONE',  ( 0.000000000000000000, 0.000000000000000000, 0.000000000000000000 ) ) ;
#11551=ORIENTED_EDGE ( 'NONE', *, *, #6261, .F. ) ;
#11571=ADVANCED_FACE ( 'NONE', ( #3512 ), #11184, .T. ) ;
#11573=VECTOR ( 'NONE', #4382, 1000.000000000000000 ) ;
#11574=VECTOR ( 'NONE', #10920, 1000.000000000000000 ) ;
#11577=DIRECTION ( 'NONE',  ( 0.000000000000000000, 0.000000000000000000, -1.000000000000000000 ) ) ;
#11578=DIRECTION ( 'NONE',  ( -0.000000000000000000, 0.000000000000000000, 1.000000000000000000 ) ) ;
#11581=ORIENTED_EDGE ( 'NONE', *, *, #1493, .T. ) ;
#11591=ORIENTED_EDGE ( 'NONE', *, *, #3642, .T. ) ;
#11596=AXIS2_PLACEMENT_3D ( 'NONE', #11093, #5347, #8344 ) ;
#11619=AXIS2_PLACEMENT_3D ( 'NONE', #9218, #5335, #4575 ) ;
#11620=DIRECTION ( 'NONE',  ( -1.000000000000000000, -0.000000000000000000, -0.000000000000000000 ) ) ;
#11625=CARTESIAN_POINT ( 'NONE',  ( 4.999999999999999112, 0.000000000000000000, 0.000000000000000000 ) ) ;
#11630=CIRCLE ( 'NONE', #4237, 27.00000000002699707 ) ;
#11633=CARTESIAN_POINT ( 'NONE',  ( 0.000000000000000000, 2.791921004064247480, 22.37914155802286942 ) ) ;
#11638=EDGE_CURVE ( 'NONE', #4328, #7808, #9387, .T. ) ;
#11642=EDGE_LOOP ( 'NONE', ( #10430, #576, #9271, #518 ) ) ;
#11654=EDGE_CURVE ( 'NONE', #12228, #11003, #3245, .T. ) ;
#11658=CIRCLE ( 'NONE', #6688, 9.600000000009604406 ) ;
#11660=DIRECTION ( 'NONE',  ( -1.000000000000000000, 0.000000000000000000, 0.000000000000000000 ) ) ;
#11665=DIRECTION ( 'NONE',  ( 0.000000000000000000, 0.000000000000000000, 1.000000000000000000 ) ) ;
#11670=VERTEX_POINT ( 'NONE', #12178 ) ;
#11681=CYLINDRICAL_SURFACE ( 'NONE', #3178, 27.00000000002699707 ) ;
#11687=ORIENTED_EDGE ( 'NONE', *, *, #979, .T. ) ;
#11689=DIRECTION ( 'NONE',  ( 0.000000000000000000, 0.9238795325112850731, 0.3826834323650938896 ) ) ;
#11694=CARTESIAN_POINT ( 'NONE',  ( 4.999999999999999112, 15.37949036966211835, 13.17168466712934105 ) ) ;
#11696=ORIENTED_EDGE ( 'NONE', *, *, #5408, .F. ) ;
#11702=DIRECTION ( 'NONE',  ( 0.000000000000000000, 0.000000000000000000, 1.000000000000000000 ) ) ;
#11703=LINE ( 'NONE', #2390, #9850 ) ;
#11705=VERTEX_POINT ( 'NONE', #10136 ) ;
#11708=ADVANCED_FACE ( 'NONE', ( #5631 ), #3634, .T. ) ;
#11711=EDGE_LOOP ( 'NONE', ( #8314, #4537, #4134, #11334 ) ) ;
#11712=CYLINDRICAL_SURFACE ( 'NONE', #9193, 9.600000000009600853 ) ;
#11717=ORIENTED_EDGE ( 'NONE', *, *, #9786, .T. ) ;
#11719=ORIENTED_EDGE ( 'NONE', *, *, #9635, .T. ) ;
#11722=DIRECTION ( 'NONE',  ( 0.000000000000000000, 0.7071067811865486830, -0.7071067811865464625 ) ) ;
#11729=CARTESIAN_POINT ( 'NONE',  ( 0.000000000000000000, 17.79862902732283914, -13.85025647830039119 ) ) ;
#11735=EDGE_CURVE ( 'NONE', #11705, #4464, #7637, .T. ) ;
#11742=LINE ( 'NONE', #7081, #6407 ) ;
#11747=FACE_OUTER_BOUND ( 'NONE', #6649, .T. ) ;
#11750=VERTEX_POINT ( 'NONE', #183 ) ;
#11759=DIRECTION ( 'NONE',  ( -1.000000000000000000, 0.000000000000000000, 0.000000000000000000 ) ) ;
#11760=CARTESIAN_POINT ( 'NONE',  ( 4.999999999999997335, 6.799999999999999822, 1.500000000000000000 ) ) ;
#11767=CARTESIAN_POINT ( 'NONE',  ( 0.000000000000000000, -19.60720892790245529, -11.14352537685195266 ) ) ;
#11771=CARTESIAN_POINT ( 'NONE',  ( 4.999999999999999112, -5.955107813822691831, 26.33508479058318485 ) ) ;
#11772=DIRECTION ( 'NONE',  ( -1.000000000000000000, 0.000000000000000000, 0.000000000000000000 ) ) ;
#11775=CARTESIAN_POINT ( 'NONE',  ( 4.999999999999999112, 0.000000000000000000, 0.000000000000000000 ) ) ;
#11779=VECTOR ( 'NONE', #8900, 1000.000000000000000 ) ;
#11787=DIRECTION ( 'NONE',  ( -1.000000000000000000, 0.000000000000000000, -0.000000000000000000 ) ) ;
#11796=VECTOR ( 'NONE', #11916, 1000.000000000000000 ) ;
#11809=AXIS2_PLACEMENT_3D ( 'NONE', #376, #4260, #10761 ) ;
#11812=CARTESIAN_POINT ( 'NONE',  ( 4.999999999999999112, 0.000000000000000000, 0.000000000000000000 ) ) ;
#11817=DIRECTION ( 'NONE',  ( 0.000000000000000000, 0.7071067811865437980, 0.7071067811865512365 ) ) ;
#11818=CARTESIAN_POINT ( 'NONE',  ( 0.000000000000000000, 4.769696007084728073, -1.500000000000000000 ) ) ;
#11820=CIRCLE ( 'NONE', #12219, 9.600000000009600853 ) ;
#11827=CIRCLE ( 'NONE', #1254, 9.600000000009600853 ) ;
#11840=ORIENTED_EDGE ( 'NONE', *, *, #10670, .F. ) ;
#11842=CARTESIAN_POINT ( 'NONE',  ( 4.999999999999999112, 19.60720892790252989, 11.14352537685181588 ) ) ;
#11844=CARTESIAN_POINT ( 'NONE',  ( 4.999999999999999112, -13.17168466712917585, -15.37949036966225513 ) ) ;
#11850=VERTEX_POINT ( 'NONE', #12303 ) ;
#11868=ADVANCED_FACE ( 'NONE', ( #11495 ), #2940, .T. ) ;
#11879=ORIENTED_EDGE ( 'NONE', *, *, #3181, .T. ) ;
#11884=CARTESIAN_POINT ( 'NONE',  ( 2.499999999999999556, 5.955107813822860585, -26.33508479058314933 ) ) ;
#11886=DIRECTION ( 'NONE',  ( -1.000000000000000000, 0.000000000000000000, 0.000000000000000000 ) ) ;
#11896=DIRECTION ( 'NONE',  ( -1.000000000000000000, 0.000000000000000000, 0.000000000000000000 ) ) ;
#11904=DIRECTION ( 'NONE',  ( 1.000000000000000000, 0.000000000000000000, 0.000000000000000000 ) ) ;
#11911=ORIENTED_EDGE ( 'NONE', *, *, #7647, .T. ) ;
#11916=DIRECTION ( 'NONE',  ( -1.000000000000000000, 0.000000000000000000, -0.000000000000000000 ) ) ;
#11917=DIRECTION ( 'NONE',  ( -1.000000000000000000, 0.000000000000000000, -0.000000000000000000 ) ) ;
#11918=CARTESIAN_POINT ( 'NONE',  ( 4.999999999999999112, 0.000000000000000000, 0.000000000000000000 ) ) ;
#11920=ORIENTED_EDGE ( 'NONE', *, *, #5934, .F. ) ;
#11926=VERTEX_POINT ( 'NONE', #5251 ) ;
#11927=FACE_OUTER_BOUND ( 'NONE', #3738, .T. ) ;
#11932=AXIS2_PLACEMENT_3D ( 'NONE', #5377, #4558, #11247 ) ;
#11933=VECTOR ( 'NONE', #3577, 1000.000000000000000 ) ;
#11935=DIRECTION ( 'NONE',  ( 0.000000000000000000, 0.000000000000000000, 1.000000000000000000 ) ) ;
#11936=DIRECTION ( 'NONE',  ( -1.000000000000000000, -0.000000000000000000, 0.000000000000000000 ) ) ;
#11940=CIRCLE ( 'NONE', #6178, 9.600000000009600853 ) ;
#11941=EDGE_LOOP ( 'NONE', ( #10257, #6465, #5383, #8745 ) ) ;
#11944=CARTESIAN_POINT ( 'NONE',  ( 4.999999999999999112, 13.17168466712950092, -15.37949036966198157 ) ) ;
#11946=CARTESIAN_POINT ( 'NONE',  ( 4.999999999999999112, -13.85025647830069317, 17.79862902732260110 ) ) ;
#11949=ORIENTED_EDGE ( 'NONE', *, *, #9376, .F. ) ;
#11950=ADVANCED_FACE ( 'NONE', ( #4245 ), #1359, .T. ) ;
#11966=CYLINDRICAL_SURFACE ( 'NONE', #6430, 27.00000000002699707 ) ;
#11968=STYLED_ITEM('',(#12391),#8661);
#11974=EDGE_CURVE ( 'NONE', #10042, #6125, #53, .T. ) ;
#11979=FACE_OUTER_BOUND ( 'NONE', #5781, .T. ) ;
#11989=DIRECTION ( 'NONE',  ( 0.000000000000000000, 0.000000000000000000, 1.000000000000000000 ) ) ;
#12003=CIRCLE ( 'NONE', #1235, 5.000000000000000000 ) ;
#12011=DIRECTION ( 'NONE',  ( -1.000000000000000000, 0.000000000000000000, 0.000000000000000000 ) ) ;
#12020=ORIENTED_EDGE ( 'NONE', *, *, #10800, .F. ) ;
#12023=CIRCLE ( 'NONE', #8817, 20.24900000002025280 ) ;
#12024=EDGE_CURVE ( 'NONE', #11497, #11670, #3351, .T. ) ;
#12025=CIRCLE ( 'NONE', #8648, 9.600000000009602630 ) ;
#12026=CARTESIAN_POINT ( 'NONE',  ( 0.000000000000000000, -26.60936692326687592, -4.576198416197529539 ) ) ;
#12030=FACE_OUTER_BOUND ( 'NONE', #8216, .T. ) ;
#12035=ORIENTED_EDGE ( 'NONE', *, *, #6071, .F. ) ;
#12040=DIRECTION ( 'NONE',  ( -1.000000000000000000, 0.000000000000000000, 0.000000000000000000 ) ) ;
#12041=DIRECTION ( 'NONE',  ( -1.000000000000000000, -0.000000000000000000, -0.000000000000000000 ) ) ;
#12046=VERTEX_POINT ( 'NONE', #4342 ) ;
#12052=DIRECTION ( 'NONE',  ( 0.000000000000000000, -0.9238795325112827417, -0.3826834323650997738 ) ) ;
#12057=AXIS2_PLACEMENT_3D ( 'NONE', #7722, #11387, #2761 ) ;
#12060=EDGE_LOOP ( 'NONE', ( #5694, #9302, #1308, #6675 ) ) ;
#12065=CARTESIAN_POINT ( 'NONE',  ( -10.00000000000000000, 0.000000000000000000, 0.000000000000000000 ) ) ;
#12069=CARTESIAN_POINT ( 'NONE',  ( 0.000000000000000000, 22.83261415639502800, 14.41081992069317508 ) ) ;
#12070=FACE_OUTER_BOUND ( 'NONE', #3237, .T. ) ;
#12071=CARTESIAN_POINT ( 'NONE',  ( 0.000000000000000000, 0.000000000000000000, 0.000000000000000000 ) ) ;
#12077=ORIENTED_EDGE ( 'NONE', *, *, #10286, .T. ) ;
#12079=ORIENTED_EDGE ( 'NONE', *, *, #9868, .T. ) ;
#12087=CARTESIAN_POINT ( 'NONE',  ( 4.999999999999999112, 26.60936692326690434, -4.576198416197341245 ) ) ;
#12088=VERTEX_POINT ( 'NONE', #9927 ) ;
#12106=DIRECTION ( 'NONE',  ( 0.000000000000000000, -0.9238795325112826307, -0.3826834323650997183 ) ) ;
#12107=ADVANCED_FACE ( 'NONE', ( #9119 ), #7984, .T. ) ;
#12111=ORIENTED_EDGE ( 'NONE', *, *, #9960, .F. ) ;
#12114=ADVANCED_FACE ( 'NONE', ( #4286 ), #7304, .T. ) ;
#12116=ORIENTED_EDGE ( 'NONE', *, *, #12266, .T. ) ;
#12123=CARTESIAN_POINT ( 'NONE',  ( 4.999999999999997335, 0.000000000000000000, 0.000000000000000000 ) ) ;
#12128=CARTESIAN_POINT ( 'NONE',  ( 5.000000000000000000, 0.000000000000000000, 1.500000000000000000 ) ) ;
#12131=FACE_OUTER_BOUND ( 'NONE', #8419, .T. ) ;
#12136=DIRECTION ( 'NONE',  ( 1.000000000000000000, 0.000000000000000000, -0.000000000000000000 ) ) ;
#12140=ORIENTED_EDGE ( 'NONE', *, *, #3947, .F. ) ;
#12146=VERTEX_POINT ( 'NONE', #8241 ) ;
#12149=AXIS2_PLACEMENT_3D ( 'NONE', #7744, #2982, #6099 ) ;
#12150=LINE ( 'NONE', #4603, #8774 ) ;
#12156=CIRCLE ( 'NONE', #3383, 27.00000000002699707 ) ;
#12161=( LENGTH_UNIT ( ) NAMED_UNIT ( * ) SI_UNIT ( .MILLI., .METRE. ) );
#12162=DIRECTION ( 'NONE',  ( -1.000000000000000000, 0.000000000000000000, 0.000000000000000000 ) ) ;
#12164=DIRECTION ( 'NONE',  ( -1.000000000000000000, -0.000000000000000000, 0.000000000000000000 ) ) ;
#12172=EDGE_CURVE ( 'NONE', #2049, #10544, #6486, .T. ) ;
#12178=CARTESIAN_POINT ( 'NONE',  ( 0.000000000000000000, 13.17168466712928598, 15.37949036966216632 ) ) ;
#12184=VECTOR ( 'NONE', #5227, 1000.000000000000000 ) ;
#12188=ORIENTED_EDGE ( 'NONE', *, *, #3476, .T. ) ;
#12189=CARTESIAN_POINT ( 'NONE',  ( 4.999999999999999112, 22.37914155802285876, -2.791921004064323864 ) ) ;
#12192=DIRECTION ( 'NONE',  ( -1.000000000000000000, 0.000000000000000000, -0.000000000000000000 ) ) ;
#12201=ADVANCED_FACE ( 'NONE', ( #10336 ), #4595, .T. ) ;
#12204=CIRCLE ( 'NONE', #4834, 9.600000000009602630 ) ;
#12206=DIRECTION ( 'NONE',  ( 0.000000000000000000, 0.000000000000000000, 1.000000000000000000 ) ) ;
#12214=EDGE_LOOP ( 'NONE', ( #8348, #6812, #5759, #3485 ) ) ;
#12219=AXIS2_PLACEMENT_3D ( 'NONE', #9041, #460, #6095 ) ;
#12222=AXIS2_PLACEMENT_3D ( 'NONE', #5903, #8023, #6019 ) ;
#12228=VERTEX_POINT ( 'NONE', #5666 ) ;
#12232=APPLICATION_CONTEXT ( 'automotive_design' ) ;
#12233=LINE ( 'NONE', #11356, #9309 ) ;
#12238=LINE ( 'NONE', #8567, #8762 ) ;
#12240=EDGE_LOOP ( 'NONE', ( #3258, #11687, #10790, #2391 ) ) ;
#12254=VERTEX_POINT ( 'NONE', #12087 ) ;
#12255=CARTESIAN_POINT ( 'NONE',  ( 0.000000000000000000, -1.561154383803364798, 20.18872947935930640 ) ) ;
#12256=CARTESIAN_POINT ( 'NONE',  ( 4.999999999999999112, -21.74405275335762155, 15.58472803277448726 ) ) ;
#12258=CYLINDRICAL_SURFACE ( 'NONE', #10170, 9.600000000009600853 ) ;
#12264=ORIENTED_EDGE ( 'NONE', *, *, #9853, .F. ) ;
#12266=EDGE_CURVE ( 'NONE', #9710, #908, #1255, .T. ) ;
#12271=CIRCLE ( 'NONE', #1502, 20.24900000002024569 ) ;
#12273=DIRECTION ( 'NONE',  ( -1.000000000000000000, -0.000000000000000000, -0.000000000000000000 ) ) ;
#12274=ORIENTED_EDGE ( 'NONE', *, *, #10447, .T. ) ;
#12277=EDGE_LOOP ( 'NONE', ( #6510, #10281, #6910, #10900 ) ) ;
#12284=ORIENTED_EDGE ( 'NONE', *, *, #3476, .F. ) ;
#12287=CARTESIAN_POINT ( 'NONE',  ( 0.000000000000000000, -4.576198416197435392, 26.60936692326689013 ) ) ;
#12290=CARTESIAN_POINT ( 'NONE',  ( 0.000000000000000000, 18.05452603534165945, 9.168210874537644273 ) ) ;
#12299=CARTESIAN_POINT ( 'NONE',  ( 4.999999999999999112, -2.791921004064401579, 22.37914155802284100 ) ) ;
#12301=EDGE_LOOP ( 'NONE', ( #12188, #1691, #8424, #10578 ) ) ;
#12303=CARTESIAN_POINT ( 'NONE',  ( 0.000000000000000000, 18.05452603534179090, -9.168210874537381372 ) ) ;
#12304=CARTESIAN_POINT ( 'NONE',  ( 4.999999999999999112, 0.000000000000000000, 0.000000000000000000 ) ) ;
#12307=CARTESIAN_POINT ( 'NONE',  ( 4.999999999999999112, 22.37914155802285876, 6.808078995945277434 ) ) ;
#12309=EDGE_CURVE ( 'NONE', #10868, #3985, #12023, .T. ) ;
#12313=EDGE_CURVE ( 'NONE', #10885, #11016, #7421, .T. ) ;
#12315=DIRECTION ( 'NONE',  ( 0.000000000000000000, 0.000000000000000000, 1.000000000000000000 ) ) ;
#12325=ORIENTED_EDGE ( 'NONE', *, *, #7477, .F. ) ;
#12326=EDGE_LOOP ( 'NONE', ( #6741, #561, #10641, #3016 ) ) ;
#12338=AXIS2_PLACEMENT_3D ( 'NONE', #6990, #6061, #9810 ) ;
#12340=ORIENTED_EDGE ( 'NONE', *, *, #10594, .T. ) ;
#12341=ORIENTED_EDGE ( 'NONE', *, *, #6845, .F. ) ;
#12343=LINE ( 'NONE', #5925, #7015 ) ;
#12347=CARTESIAN_POINT ( 'NONE',  ( 4.999999999999999112, 0.000000000000000000, 0.000000000000000000 ) ) ;
#12349=ORIENTED_EDGE ( 'NONE', *, *, #5258, .T. ) ;
#12351=SURFACE_STYLE_FILL_AREA ( #10299 ) ;
#12385=COLOUR_RGB('Sky Blue',0.24,0.69,0.87);
#12386=FILL_AREA_STYLE_COLOUR('',#12385);
#12387=FILL_AREA_STYLE('',(#12386));
#12388=SURFACE_STYLE_FILL_AREA(#12387);
#12389=SURFACE_SIDE_STYLE('',(#12388));
#12390=SURFACE_STYLE_USAGE(.BOTH.,#12389);
#12391=PRESENTATION_STYLE_ASSIGNMENT((#12390));
ENDSEC;
END-ISO-10303-21;
